ISO-10303-21;
HEADER;
FILE_DESCRIPTION (('STEP AP214'),
    '1' );
FILE_NAME ('Drive End Plate.step',
    '2026-10-22T18:53:08',
    ( '' ),
    ( '' ),
    'SwSTEP 2.0',
    'SolidWorks 2025',
    '' );
FILE_SCHEMA (( 'AUTOMOTIVE_DESIGN' ));
ENDSEC;

DATA;
#1=EDGE_CURVE ( 'NONE', #11499, #20840, #16615, .T. ) ;
#31=FACE_OUTER_BOUND ( 'NONE', #11756, .T. ) ;
#34=ORIENTED_EDGE ( 'NONE', *, *, #12812, .F. ) ;
#46=ORIENTED_EDGE ( 'NONE', *, *, #10714, .T. ) ;
#47=VERTEX_POINT ( 'NONE', #16968 ) ;
#52=ORIENTED_EDGE ( 'NONE', *, *, #5845, .F. ) ;
#56=CARTESIAN_POINT ( 'NONE',  ( 35.99999999999992184, -60.00000000000000000, 0.000000000000000000 ) ) ;
#62=CARTESIAN_POINT ( 'NONE',  ( -28.99999999999999645, -29.50000000000000000, 12.50000000000000000 ) ) ;
#64=DIRECTION ( 'NONE',  ( -0.000000000000000000, 0.000000000000000000, -1.000000000000000000 ) ) ;
#84=LINE ( 'NONE', #7029, #8324 ) ;
#88=ORIENTED_EDGE ( 'NONE', *, *, #16385, .T. ) ;
#104=( NAMED_UNIT ( * ) PLANE_ANGLE_UNIT ( ) SI_UNIT ( $, .RADIAN. ) );
#109=ORIENTED_EDGE ( 'NONE', *, *, #14382, .F. ) ;
#125=LINE ( 'NONE', #22458, #18476 ) ;
#126=ORIENTED_EDGE ( 'NONE', *, *, #5435, .F. ) ;
#136=AXIS2_PLACEMENT_3D ( 'NONE', #11343, #23969, #18827 ) ;
#138=CIRCLE ( 'NONE', #3244, 1.500000000000000000 ) ;
#139=EDGE_CURVE ( 'NONE', #6140, #16103, #754, .T. ) ;
#146=DIRECTION ( 'NONE',  ( -1.000000000000000000, 0.000000000000000000, -0.000000000000000000 ) ) ;
#148=AXIS2_PLACEMENT_3D ( 'NONE', #10109, #500, #7919 ) ;
#153=AXIS2_PLACEMENT_3D ( 'NONE', #4765, #13942, #9753 ) ;
#158=AXIS2_PLACEMENT_3D ( 'NONE', #9827, #13523, #460 ) ;
#163=DIRECTION ( 'NONE',  ( -0.000000000000000000, -0.000000000000000000, -1.000000000000000000 ) ) ;
#168=DIRECTION ( 'NONE',  ( -0.7089874389501492624, -0.7052211081716913688, 0.000000000000000000 ) ) ;
#169=ORIENTED_EDGE ( 'NONE', *, *, #19806, .T. ) ;
#187=CARTESIAN_POINT ( 'NONE',  ( 39.50000000000000000, 15.50000000000000533, 19.70000000000000284 ) ) ;
#189=LINE ( 'NONE', #16870, #10641 ) ;
#200=AXIS2_PLACEMENT_3D ( 'NONE', #19506, #8617, #6317 ) ;
#205=DIRECTION ( 'NONE',  ( 1.360567432138674300E-16, -1.000000000000000000, 0.000000000000000000 ) ) ;
#207=CARTESIAN_POINT ( 'NONE',  ( 35.99999999999999289, -51.00000000000000711, 0.5000000000000000000 ) ) ;
#212=AXIS2_PLACEMENT_3D ( 'NONE', #21682, #3240, #1302 ) ;
#213=DIRECTION ( 'NONE',  ( 1.000000000000000000, 0.000000000000000000, 0.000000000000000000 ) ) ;
#217=ADVANCED_FACE ( 'NONE', ( #8123 ), #8920, .F. ) ;
#228=ORIENTED_EDGE ( 'NONE', *, *, #4150, .T. ) ;
#231=ORIENTED_EDGE ( 'NONE', *, *, #12229, .F. ) ;
#235=AXIS2_PLACEMENT_3D ( 'NONE', #20947, #21054, #11640 ) ;
#247=EDGE_CURVE ( 'NONE', #17382, #16656, #7759, .T. ) ;
#253=AXIS2_PLACEMENT_3D ( 'NONE', #18403, #14486, #19889 ) ;
#256=VECTOR ( 'NONE', #12691, 1000.000000000000000 ) ;
#261=ORIENTED_EDGE ( 'NONE', *, *, #13949, .F. ) ;
#268=EDGE_CURVE ( 'NONE', #16760, #20840, #2329, .T. ) ;
#271=AXIS2_PLACEMENT_3D ( 'NONE', #14619, #3409, #18293 ) ;
#275=EDGE_CURVE ( 'NONE', #13326, #18344, #10190, .T. ) ;
#278=DIRECTION ( 'NONE',  ( -0.000000000000000000, -0.000000000000000000, 1.000000000000000000 ) ) ;
#286=CARTESIAN_POINT ( 'NONE',  ( -40.23082370883260239, 29.50000000000000711, -3.000000000000000000 ) ) ;
#287=ORIENTED_EDGE ( 'NONE', *, *, #13188, .T. ) ;
#290=CARTESIAN_POINT ( 'NONE',  ( 2.024999999999999911, 45.00000000000000000, -3.000000000000000000 ) ) ;
#305=PLANE ( 'NONE',  #884 ) ;
#312=ORIENTED_EDGE ( 'NONE', *, *, #2580, .F. ) ;
#333=DIRECTION ( 'NONE',  ( -0.7052211081716905916, 0.7089874389501501506, 0.000000000000000000 ) ) ;
#337=DIRECTION ( 'NONE',  ( 1.000000000000000000, 0.000000000000000000, 0.000000000000000000 ) ) ;
#378=FACE_BOUND ( 'NONE', #14789, .T. ) ;
#381=ORIENTED_EDGE ( 'NONE', *, *, #16023, .T. ) ;
#393=ORIENTED_EDGE ( 'NONE', *, *, #6106, .F. ) ;
#397=CYLINDRICAL_SURFACE ( 'NONE', #14885, 1.499999999999998002 ) ;
#417=FACE_BOUND ( 'NONE', #11319, .T. ) ;
#420=FACE_OUTER_BOUND ( 'NONE', #7295, .T. ) ;
#429=ORIENTED_EDGE ( 'NONE', *, *, #19468, .F. ) ;
#458=DIRECTION ( 'NONE',  ( 0.000000000000000000, 0.000000000000000000, -1.000000000000000000 ) ) ;
#460=DIRECTION ( 'NONE',  ( 1.000000000000000000, 0.000000000000000000, 0.000000000000000000 ) ) ;
#464=ORIENTED_EDGE ( 'NONE', *, *, #22760, .F. ) ;
#481=ORIENTED_EDGE ( 'NONE', *, *, #11661, .F. ) ;
#500=DIRECTION ( 'NONE',  ( 0.000000000000000000, 1.000000000000000000, 0.000000000000000000 ) ) ;
#501=DIRECTION ( 'NONE',  ( -1.000000000000000000, 0.000000000000000000, 0.000000000000000000 ) ) ;
#504=VECTOR ( 'NONE', #5212, 1000.000000000000114 ) ;
#511=AXIS2_PLACEMENT_3D ( 'NONE', #14794, #18599, #11234 ) ;
#519=DIRECTION ( 'NONE',  ( 0.7089874389501492624, 0.7052211081716913688, 0.000000000000000000 ) ) ;
#523=LINE ( 'NONE', #2717, #14616 ) ;
#531=AXIS2_PLACEMENT_3D ( 'NONE', #1963, #11466, #5767 ) ;
#538=DIRECTION ( 'NONE',  ( -0.000000000000000000, -0.000000000000000000, -1.000000000000000000 ) ) ;
#539=CARTESIAN_POINT ( 'NONE',  ( -17.25000000000000000, 15.50000000000000000, 14.70000000000000284 ) ) ;
#541=CARTESIAN_POINT ( 'NONE',  ( 29.00000000000000355, -29.50000000000000000, -3.000000000000000000 ) ) ;
#542=ORIENTED_EDGE ( 'NONE', *, *, #18708, .T. ) ;
#543=CYLINDRICAL_SURFACE ( 'NONE', #962, 5.000000000000000888 ) ;
#545=ORIENTED_EDGE ( 'NONE', *, *, #20956, .F. ) ;
#549=ORIENTED_EDGE ( 'NONE', *, *, #21450, .T. ) ;
#550=AXIS2_PLACEMENT_3D ( 'NONE', #11975, #19444, #2723 ) ;
#559=LINE ( 'NONE', #6165, #2084 ) ;
#561=ORIENTED_EDGE ( 'NONE', *, *, #17545, .F. ) ;
#563=LINE ( 'NONE', #19228, #13900 ) ;
#564=CARTESIAN_POINT ( 'NONE',  ( 0.000000000000000000, -45.00000000000000000, -8.673617379884035472E-16 ) ) ;
#574=CARTESIAN_POINT ( 'NONE',  ( -41.73082370883260239, 27.62204025492845361, -3.000000000000000000 ) ) ;
#583=ORIENTED_EDGE ( 'NONE', *, *, #20637, .F. ) ;
#599=LINE ( 'NONE', #9963, #8749 ) ;
#606=EDGE_CURVE ( 'NONE', #18123, #12662, #6674, .T. ) ;
#621=DIRECTION ( 'NONE',  ( -0.000000000000000000, -0.000000000000000000, -1.000000000000000000 ) ) ;
#631=ORIENTED_EDGE ( 'NONE', *, *, #5431, .T. ) ;
#633=CIRCLE ( 'NONE', #6869, 49.99999999999998579 ) ;
#648=DIRECTION ( 'NONE',  ( -1.000000000000000000, 0.000000000000000000, 0.000000000000000000 ) ) ;
#649=AXIS2_PLACEMENT_3D ( 'NONE', #23008, #23137, #15541 ) ;
#662=CARTESIAN_POINT ( 'NONE',  ( -41.73082370883258108, -29.50000000000000711, 0.000000000000000000 ) ) ;
#664=CARTESIAN_POINT ( 'NONE',  ( -40.66734255040736201, -26.56420859267092283, -1.500000000000000000 ) ) ;
#665=CARTESIAN_POINT ( 'NONE',  ( 0.000000000000000000, 15.50000000000000000, 16.70000000000000284 ) ) ;
#670=CARTESIAN_POINT ( 'NONE',  ( 30.68762588338048403, 45.64284848299539732, 0.000000000000000000 ) ) ;
#673=CARTESIAN_POINT ( 'NONE',  ( -36.00000000000000711, -51.00000000000000711, 0.5000000000000000000 ) ) ;
#680=ORIENTED_EDGE ( 'NONE', *, *, #17441, .F. ) ;
#685=CARTESIAN_POINT ( 'NONE',  ( -45.00000000000001421, 50.99999999999992184, 0.000000000000000000 ) ) ;
#696=ORIENTED_EDGE ( 'NONE', *, *, #18309, .T. ) ;
#703=CARTESIAN_POINT ( 'NONE',  ( 30.68762588338048403, 45.64284848299539732, -1.500000000000000000 ) ) ;
#705=ADVANCED_FACE ( 'NONE', ( #15132 ), #397, .F. ) ;
#712=EDGE_CURVE ( 'NONE', #10867, #18287, #7477, .T. ) ;
#724=DIRECTION ( 'NONE',  ( -0.7052211081716915908, 0.7089874389501490404, -0.000000000000000000 ) ) ;
#738=CARTESIAN_POINT ( 'NONE',  ( 29.00000000000000355, -29.50000000000000000, -2.224999999999995204 ) ) ;
#743=PLANE ( 'NONE',  #19572 ) ;
#747=VERTEX_POINT ( 'NONE', #14052 ) ;
#754=CIRCLE ( 'NONE', #12821, 1.500000000000000000 ) ;
#764=FACE_BOUND ( 'NONE', #23465, .T. ) ;
#773=ORIENTED_EDGE ( 'NONE', *, *, #14811, .T. ) ;
#778=CARTESIAN_POINT ( 'NONE',  ( 28.99999999999998579, -29.49999999999999645, -1.500000000000000000 ) ) ;
#779=VERTEX_POINT ( 'NONE', #12211 ) ;
#784=DIRECTION ( 'NONE',  ( -0.000000000000000000, -0.000000000000000000, -1.000000000000000000 ) ) ;
#807=DIRECTION ( 'NONE',  ( -0.000000000000000000, -0.000000000000000000, -1.000000000000000000 ) ) ;
#813=LINE ( 'NONE', #4975, #3726 ) ;
#814=DIRECTION ( 'NONE',  ( -0.000000000000000000, -0.000000000000000000, 1.000000000000000000 ) ) ;
#822=ORIENTED_EDGE ( 'NONE', *, *, #9732, .F. ) ;
#830=DIRECTION ( 'NONE',  ( -5.501724186093582121E-16, 1.000000000000000000, 0.000000000000000000 ) ) ;
#833=DIRECTION ( 'NONE',  ( -0.000000000000000000, -1.000000000000000000, -0.000000000000000000 ) ) ;
#838=CYLINDRICAL_SURFACE ( 'NONE', #3638, 11.23082370883260417 ) ;
#839=CARTESIAN_POINT ( 'NONE',  ( -28.99999999999998579, -29.50000000000000711, -3.000000000000000000 ) ) ;
#858=AXIS2_PLACEMENT_3D ( 'NONE', #13331, #538, #11614 ) ;
#860=ORIENTED_EDGE ( 'NONE', *, *, #16308, .F. ) ;
#864=FACE_OUTER_BOUND ( 'NONE', #3660, .T. ) ;
#866=DIRECTION ( 'NONE',  ( -0.000000000000000000, -0.000000000000000000, 1.000000000000000000 ) ) ;
#871=DIRECTION ( 'NONE',  ( -0.000000000000000000, -0.000000000000000000, -1.000000000000000000 ) ) ;
#883=PLANE ( 'NONE',  #8037 ) ;
#884=AXIS2_PLACEMENT_3D ( 'NONE', #22876, #11979, #2243 ) ;
#890=ORIENTED_EDGE ( 'NONE', *, *, #7196, .T. ) ;
#896=CYLINDRICAL_SURFACE ( 'NONE', #9627, 49.99999999999998579 ) ;
#903=ORIENTED_EDGE ( 'NONE', *, *, #21850, .F. ) ;
#910=VERTEX_POINT ( 'NONE', #21750 ) ;
#927=ORIENTED_EDGE ( 'NONE', *, *, #22597, .T. ) ;
#938=AXIS2_PLACEMENT_3D ( 'NONE', #22239, #12943, #5510 ) ;
#944=VECTOR ( 'NONE', #4341, 1000.000000000000000 ) ;
#961=ADVANCED_FACE ( 'NONE', ( #7323 ), #5040, .F. ) ;
#962=AXIS2_PLACEMENT_3D ( 'NONE', #19930, #8691, #23609 ) ;
#978=VERTEX_POINT ( 'NONE', #11083 ) ;
#986=DIRECTION ( 'NONE',  ( -0.000000000000000000, -0.000000000000000000, 1.000000000000000000 ) ) ;
#995=ORIENTED_EDGE ( 'NONE', *, *, #13482, .T. ) ;
#1004=AXIS2_PLACEMENT_3D ( 'NONE', #17938, #1109, #3055 ) ;
#1013=SHAPE_REPRESENTATION ( 'Drive End Plate', ( #8005 ), #15828 ) ;
#1019=EDGE_CURVE ( 'NONE', #16520, #17900, #9810, .T. ) ;
#1022=ORIENTED_EDGE ( 'NONE', *, *, #19910, .T. ) ;
#1028=ORIENTED_EDGE ( 'NONE', *, *, #11588, .F. ) ;
#1037=DIRECTION ( 'NONE',  ( 0.000000000000000000, 0.000000000000000000, 1.000000000000000000 ) ) ;
#1048=ORIENTED_EDGE ( 'NONE', *, *, #6379, .T. ) ;
#1049=ORIENTED_EDGE ( 'NONE', *, *, #15730, .F. ) ;
#1058=EDGE_LOOP ( 'NONE', ( #23023, #11672 ) ) ;
#1061=ORIENTED_EDGE ( 'NONE', *, *, #3350, .T. ) ;
#1063=AXIS2_PLACEMENT_3D ( 'NONE', #9729, #17186, #15480 ) ;
#1064=DIRECTION ( 'NONE',  ( -0.000000000000000000, -0.000000000000000000, -1.000000000000000000 ) ) ;
#1074=AXIS2_PLACEMENT_3D ( 'NONE', #10333, #12286, #19386 ) ;
#1088=CARTESIAN_POINT ( 'NONE',  ( -35.99999999999995026, 59.99999999999998579, 12.50000000000000000 ) ) ;
#1091=VERTEX_POINT ( 'NONE', #11199 ) ;
#1099=LINE ( 'NONE', #2672, #20811 ) ;
#1109=DIRECTION ( 'NONE',  ( -4.625929269271481378E-15, 1.000000000000000000, -2.139922160430260066E-29 ) ) ;
#1114=ORIENTED_EDGE ( 'NONE', *, *, #14057, .T. ) ;
#1116=FACE_OUTER_BOUND ( 'NONE', #23887, .T. ) ;
#1130=ORIENTED_EDGE ( 'NONE', *, *, #18210, .F. ) ;
#1133=VECTOR ( 'NONE', #6566, 1000.000000000000000 ) ;
#1146=CYLINDRICAL_SURFACE ( 'NONE', #21356, 8.000000000000000000 ) ;
#1153=CARTESIAN_POINT ( 'NONE',  ( -17.25000000000000000, 15.50000000000000000, 7.700000000000001954 ) ) ;
#1157=ORIENTED_EDGE ( 'NONE', *, *, #6133, .T. ) ;
#1162=EDGE_CURVE ( 'NONE', #6139, #5924, #8274, .T. ) ;
#1165=EDGE_LOOP ( 'NONE', ( #10490, #5286, #15472, #18274 ) ) ;
#1166=CIRCLE ( 'NONE', #11647, 2.024999999999999911 ) ;
#1169=ORIENTED_EDGE ( 'NONE', *, *, #3377, .T. ) ;
#1170=LINE ( 'NONE', #6896, #17807 ) ;
#1173=ORIENTED_EDGE ( 'NONE', *, *, #12448, .F. ) ;
#1175=CARTESIAN_POINT ( 'NONE',  ( 40.66734255040738333, 26.56420859267091217, -3.000000000000000000 ) ) ;
#1176=ORIENTED_EDGE ( 'NONE', *, *, #20506, .F. ) ;
#1186=CYLINDRICAL_SURFACE ( 'NONE', #8299, 1.500000000000001332 ) ;
#1204=DIRECTION ( 'NONE',  ( 0.000000000000000000, 1.000000000000000000, 0.000000000000000000 ) ) ;
#1211=EDGE_CURVE ( 'NONE', #16656, #17382, #17580, .T. ) ;
#1225=LINE ( 'NONE', #11812, #16572 ) ;
#1229=ADVANCED_FACE ( 'NONE', ( #1477 ), #18184, .T. ) ;
#1233=EDGE_CURVE ( 'NONE', #19491, #18312, #7052, .T. ) ;
#1253=EDGE_CURVE ( 'NONE', #1785, #19039, #20133, .T. ) ;
#1273=DIRECTION ( 'NONE',  ( -0.000000000000000000, -0.000000000000000000, -1.000000000000000000 ) ) ;
#1291=VECTOR ( 'NONE', #14403, 1000.000000000000114 ) ;
#1294=( BOUNDED_CURVE ( )  B_SPLINE_CURVE ( 3, ( #3752, #12733, #3865, #7391 ),
 .UNSPECIFIED., .F., .T. ) 
 B_SPLINE_CURVE_WITH_KNOTS ( ( 4, 4 ),
 ( 3.141592653589793116, 4.712388980384689674 ),
 .UNSPECIFIED. ) 
 CURVE ( )  GEOMETRIC_REPRESENTATION_ITEM ( )  RATIONAL_B_SPLINE_CURVE ( ( 1.000000000000000000, 0.8047378541243649375, 0.8047378541243649375, 1.000000000000000000 ) ) 
 REPRESENTATION_ITEM ( '' )  );
#1295=DIRECTION ( 'NONE',  ( -0.000000000000000000, -0.000000000000000000, -1.000000000000000000 ) ) ;
#1302=DIRECTION ( 'NONE',  ( 1.000000000000000000, 0.000000000000000000, 0.000000000000000000 ) ) ;
#1305=AXIS2_PLACEMENT_3D ( 'NONE', #12854, #11502, #22623 ) ;
#1311=VECTOR ( 'NONE', #15595, 1000.000000000000000 ) ;
#1320=DIRECTION ( 'NONE',  ( -0.5579568342432784656, 0.8298699724181003434, 0.000000000000000000 ) ) ;
#1328=CIRCLE ( 'NONE', #531, 4.249999999999996447 ) ;
#1329=CIRCLE ( 'NONE', #212, 11.23082370883260417 ) ;
#1332=CARTESIAN_POINT ( 'NONE',  ( -40.50000000000000711, 50.99999999999999289, 12.50000000000000000 ) ) ;
#1333=CYLINDRICAL_SURFACE ( 'NONE', #18013, 5.000000000000000888 ) ;
#1339=FACE_BOUND ( 'NONE', #4202, .T. ) ;
#1346=CIRCLE ( 'NONE', #8722, 5.025000000000002132 ) ;
#1361=ORIENTED_EDGE ( 'NONE', *, *, #5824, .F. ) ;
#1378=ORIENTED_EDGE ( 'NONE', *, *, #23194, .F. ) ;
#1380=VECTOR ( 'NONE', #14711, 1000.000000000000000 ) ;
#1390=EDGE_LOOP ( 'NONE', ( #23022, #7636, #6946, #12939 ) ) ;
#1396=AXIS2_PLACEMENT_3D ( 'NONE', #10949, #23697, #22335 ) ;
#1400=DIRECTION ( 'NONE',  ( -1.000000000000000000, 0.000000000000000000, 0.000000000000000000 ) ) ;
#1401=CARTESIAN_POINT ( 'NONE',  ( 27.99999999999998934, -51.00000000000000711, 0.5000000000000000000 ) ) ;
#1404=CARTESIAN_POINT ( 'NONE',  ( -45.00000000000001421, 50.99999999999992184, 12.50000000000000000 ) ) ;
#1412=AXIS2_PLACEMENT_3D ( 'NONE', #17511, #10058, #4724 ) ;
#1419=CARTESIAN_POINT ( 'NONE',  ( -40.23082370883257397, -29.50000000000000711, -3.000000000000000000 ) ) ;
#1425=CYLINDRICAL_SURFACE ( 'NONE', #2968, 1.499999999999998002 ) ;
#1429=CARTESIAN_POINT ( 'NONE',  ( 34.02500000000000568, -29.50000000000000000, -3.000000000000000000 ) ) ;
#1430=DIRECTION ( 'NONE',  ( -1.000000000000000000, 0.000000000000000000, 0.000000000000000000 ) ) ;
#1441=ORIENTED_EDGE ( 'NONE', *, *, #11534, .T. ) ;
#1444=SHAPE_DEFINITION_REPRESENTATION ( #8854, #1013 ) ;
#1462=CYLINDRICAL_SURFACE ( 'NONE', #4833, 1.499999999999994449 ) ;
#1470=VERTEX_POINT ( 'NONE', #24055 ) ;
#1477=FACE_OUTER_BOUND ( 'NONE', #14795, .T. ) ;
#1478=CARTESIAN_POINT ( 'NONE',  ( -36.00000000000001421, 50.99999999999999289, 0.5000000000000004441 ) ) ;
#1485=VERTEX_POINT ( 'NONE', #3449 ) ;
#1495=CARTESIAN_POINT ( 'NONE',  ( -30.68762588338046982, -45.64284848299540442, -1.500000000000000000 ) ) ;
#1498=EDGE_CURVE ( 'NONE', #1766, #13946, #15222, .T. ) ;
#1501=DIRECTION ( 'NONE',  ( 1.000000000000000000, 0.000000000000000000, 0.000000000000000000 ) ) ;
#1513=CARTESIAN_POINT ( 'NONE',  ( -27.89784171216405895, 41.49349862090491570, -3.000000000000000000 ) ) ;
#1516=EDGE_CURVE ( 'NONE', #2260, #13127, #5517, .T. ) ;
#1519=FACE_OUTER_BOUND ( 'NONE', #6255, .T. ) ;
#1524=ORIENTED_EDGE ( 'NONE', *, *, #18346, .F. ) ;
#1530=CARTESIAN_POINT ( 'NONE',  ( -30.68762588338046982, -45.64284848299540442, 0.000000000000000000 ) ) ;
#1535=ADVANCED_FACE ( 'NONE', ( #10751 ), #16033, .F. ) ;
#1540=CARTESIAN_POINT ( 'NONE',  ( 0.000000000000000000, 0.000000000000000000, -3.000000000000000000 ) ) ;
#1542=DIRECTION ( 'NONE',  ( -0.7089874389501492624, 0.7052211081716913688, 0.000000000000000000 ) ) ;
#1549=VERTEX_POINT ( 'NONE', #6112 ) ;
#1558=AXIS2_PLACEMENT_3D ( 'NONE', #10312, #2519, #8487 ) ;
#1568=DIRECTION ( 'NONE',  ( -0.000000000000000000, -0.000000000000000000, -1.000000000000000000 ) ) ;
#1582=CARTESIAN_POINT ( 'NONE',  ( 15.00000000000000355, 15.50000000000000000, 19.70000000000000284 ) ) ;
#1612=CARTESIAN_POINT ( 'NONE',  ( 44.99999999999998579, 50.99999999999992184, 0.000000000000000000 ) ) ;
#1613=DIRECTION ( 'NONE',  ( -1.000000000000000000, 0.000000000000000000, 0.000000000000000000 ) ) ;
#1619=CARTESIAN_POINT ( 'NONE',  ( -36.00000000000000711, -51.00000000000000711, 0.5000000000000000000 ) ) ;
#1620=CARTESIAN_POINT ( 'NONE',  ( 3.890962118697714531E-15, 15.50000000000000000, 19.70000000000000284 ) ) ;
#1634=DIRECTION ( 'NONE',  ( 1.000000000000000000, 0.000000000000000000, 0.000000000000000000 ) ) ;
#1642=VECTOR ( 'NONE', #14147, 1000.000000000000000 ) ;
#1644=DIRECTION ( 'NONE',  ( 1.000000000000000000, 0.000000000000000000, 0.000000000000000000 ) ) ;
#1647=DIRECTION ( 'NONE',  ( 0.000000000000000000, 0.000000000000000000, 1.000000000000000000 ) ) ;
#1655=AXIS2_PLACEMENT_3D ( 'NONE', #8868, #3266, #6936 ) ;
#1659=ADVANCED_FACE ( 'NONE', ( #1116 ), #17559, .T. ) ;
#1668=DIRECTION ( 'NONE',  ( 0.1039766011667122986, 0.9945797436152711279, 0.000000000000000000 ) ) ;
#1676=ORIENTED_EDGE ( 'NONE', *, *, #9580, .F. ) ;
#1686=DIRECTION ( 'NONE',  ( -1.000000000000000000, 0.000000000000000000, -0.000000000000000000 ) ) ;
#1687=CONICAL_SURFACE ( 'NONE', #23891, 5.025000000000002132, 0.7853981633974482790 ) ;
#1698=CARTESIAN_POINT ( 'NONE',  ( 33.24999999999999289, 29.50000000000000000, 14.00000000000000178 ) ) ;
#1700=EDGE_CURVE ( 'NONE', #15766, #14863, #16800, .T. ) ;
#1703=CIRCLE ( 'NONE', #3643, 5.025000000000002132 ) ;
#1704=DIRECTION ( 'NONE',  ( -1.000000000000000000, 0.000000000000000000, 0.000000000000000000 ) ) ;
#1713=VECTOR ( 'NONE', #5900, 1000.000000000000000 ) ;
#1721=VECTOR ( 'NONE', #15643, 1000.000000000000000 ) ;
#1725=EDGE_CURVE ( 'NONE', #18312, #13651, #12521, .T. ) ;
#1759=VERTEX_POINT ( 'NONE', #56 ) ;
#1760=CARTESIAN_POINT ( 'NONE',  ( -40.23082370883257397, -29.50000000000000711, -1.500000000000000000 ) ) ;
#1766=VERTEX_POINT ( 'NONE', #22389 ) ;
#1774=FACE_BOUND ( 'NONE', #5128, .T. ) ;
#1785=VERTEX_POINT ( 'NONE', #3471 ) ;
#1801=EDGE_CURVE ( 'NONE', #8729, #12142, #22144, .T. ) ;
#1802=ORIENTED_EDGE ( 'NONE', *, *, #5103, .T. ) ;
#1807=CARTESIAN_POINT ( 'NONE',  ( -36.00000000000000711, -51.00000000000000711, 0.5000000000000004441 ) ) ;
#1814=VECTOR ( 'NONE', #14793, 1000.000000000000000 ) ;
#1816=ADVANCED_FACE ( 'NONE', ( #18965 ), #9766, .F. ) ;
#1818=VERTEX_POINT ( 'NONE', #11858 ) ;
#1826=CARTESIAN_POINT ( 'NONE',  ( 44.99999999999998579, 50.99999999999992184, 12.50000000000000000 ) ) ;
#1841=EDGE_LOOP ( 'NONE', ( #5037, #6701, #16418, #6702 ) ) ;
#1843=DIRECTION ( 'NONE',  ( -1.000000000000000000, 0.000000000000000000, 0.000000000000000000 ) ) ;
#1854=DIRECTION ( 'NONE',  ( 0.7089874389501492624, 0.7052211081716913688, 0.000000000000000000 ) ) ;
#1857=EDGE_CURVE ( 'NONE', #978, #747, #19195, .T. ) ;
#1862=CARTESIAN_POINT ( 'NONE',  ( 28.99999999999999645, 29.50000000000000000, 16.55365763086713216 ) ) ;
#1863=VERTEX_POINT ( 'NONE', #19446 ) ;
#1870=ORIENTED_EDGE ( 'NONE', *, *, #9624, .F. ) ;
#1878=VERTEX_POINT ( 'NONE', #14301 ) ;
#1879=DIRECTION ( 'NONE',  ( -0.5579568342432823513, 0.8298699724180977899, 0.000000000000000000 ) ) ;
#1887=AXIS2_PLACEMENT_3D ( 'NONE', #13091, #16993, #1879 ) ;
#1890=DIRECTION ( 'NONE',  ( 0.9945797436152715720, -0.1039766011667100365, 0.000000000000000000 ) ) ;
#1893=DIRECTION ( 'NONE',  ( 1.000000000000000000, 0.000000000000000000, 0.000000000000000000 ) ) ;
#1908=DIRECTION ( 'NONE',  ( -0.000000000000000000, -0.000000000000000000, -1.000000000000000000 ) ) ;
#1916=CARTESIAN_POINT ( 'NONE',  ( 3.890962118697714531E-15, 15.50000000000000000, 19.70000000000000284 ) ) ;
#1921=VERTEX_POINT ( 'NONE', #15777 ) ;
#1924=ORIENTED_EDGE ( 'NONE', *, *, #2580, .T. ) ;
#1931=CARTESIAN_POINT ( 'NONE',  ( 35.99999999999999289, -51.00000000000000711, 0.5000000000000000000 ) ) ;
#1934=ADVANCED_FACE ( 'NONE', ( #10138 ), #9258, .F. ) ;
#1943=CIRCLE ( 'NONE', #15569, 4.499999999999997335 ) ;
#1945=ORIENTED_EDGE ( 'NONE', *, *, #4677, .F. ) ;
#1952=VERTEX_POINT ( 'NONE', #12089 ) ;
#1957=EDGE_LOOP ( 'NONE', ( #3955, #1048, #9655, #3274 ) ) ;
#1963=CARTESIAN_POINT ( 'NONE',  ( 29.00000000000000355, -29.50000000000000000, 12.50000000000000000 ) ) ;
#1965=CYLINDRICAL_SURFACE ( 'NONE', #13252, 17.25000000000000000 ) ;
#1980=FACE_OUTER_BOUND ( 'NONE', #18162, .T. ) ;
#1985=DIRECTION ( 'NONE',  ( -0.000000000000000000, -0.000000000000000000, 1.000000000000000000 ) ) ;
#1989=DIRECTION ( 'NONE',  ( 0.8571673007021121116, 1.049727191138618449E-16, -0.5150380749100544886 ) ) ;
#1992=DIRECTION ( 'NONE',  ( -0.8571673007021118895, 0.000000000000000000, -0.5150380749100549327 ) ) ;
#2004=ORIENTED_EDGE ( 'NONE', *, *, #1700, .T. ) ;
#2006=AXIS2_PLACEMENT_3D ( 'NONE', #14038, #10373, #12190 ) ;
#2010=EDGE_CURVE ( 'NONE', #15940, #22890, #6571, .T. ) ;
#2018=CARTESIAN_POINT ( 'NONE',  ( 3.890962118697714531E-15, 15.50000000000000000, 14.70000000000000284 ) ) ;
#2024=DIRECTION ( 'NONE',  ( 0.000000000000000000, 0.000000000000000000, 1.000000000000000000 ) ) ;
#2025=CIRCLE ( 'NONE', #17224, 8.000000000000000000 ) ;
#2030=AXIS2_PLACEMENT_3D ( 'NONE', #9842, #15202, #20975 ) ;
#2032=AXIS2_PLACEMENT_3D ( 'NONE', #6638, #3091, #14071 ) ;
#2039=ORIENTED_EDGE ( 'NONE', *, *, #22915, .T. ) ;
#2047=CIRCLE ( 'NONE', #18428, 11.23082370883260417 ) ;
#2059=ORIENTED_EDGE ( 'NONE', *, *, #2375, .T. ) ;
#2060=LINE ( 'NONE', #9357, #23600 ) ;
#2064=VECTOR ( 'NONE', #6177, 1000.000000000000000 ) ;
#2070=DIRECTION ( 'NONE',  ( -1.000000000000000000, -1.776356839400250465E-15, 0.000000000000000000 ) ) ;
#2071=AXIS2_PLACEMENT_3D ( 'NONE', #670, #21877, #7103 ) ;
#2081=AXIS2_PLACEMENT_3D ( 'NONE', #6395, #8330, #13836 ) ;
#2084=VECTOR ( 'NONE', #22635, 1000.000000000000000 ) ;
#2086=LINE ( 'NONE', #7683, #6615 ) ;
#2099=DIRECTION ( 'NONE',  ( 0.7052211081716914798, -0.7089874389501492624, 0.000000000000000000 ) ) ;
#2107=DIRECTION ( 'NONE',  ( -1.000000000000000000, 0.000000000000000000, 0.000000000000000000 ) ) ;
#2109=CIRCLE ( 'NONE', #5243, 3.500000000000003109 ) ;
#2117=DIRECTION ( 'NONE',  ( -0.000000000000000000, -0.000000000000000000, -1.000000000000000000 ) ) ;
#2120=FACE_BOUND ( 'NONE', #9016, .T. ) ;
#2123=PLANE ( 'NONE',  #21632 ) ;
#2127=CARTESIAN_POINT ( 'NONE',  ( -36.00000000000001421, 50.99999999999999289, 12.50000000000000000 ) ) ;
#2131=VERTEX_POINT ( 'NONE', #18800 ) ;
#2141=CARTESIAN_POINT ( 'NONE',  ( 27.99999999999998934, 50.99999999999999289, 0.5000000000000000000 ) ) ;
#2148=DIRECTION ( 'NONE',  ( 1.000000000000000000, 0.000000000000000000, 0.000000000000000000 ) ) ;
#2157=AXIS2_PLACEMENT_3D ( 'NONE', #12068, #14047, #19541 ) ;
#2175=CARTESIAN_POINT ( 'NONE',  ( 29.00000000000000000, 29.50000000000000000, -3.000000000000000000 ) ) ;
#2180=CARTESIAN_POINT ( 'NONE',  ( -44.00000000000001421, 50.99999999999999289, 0.5000000000000000000 ) ) ;
#2182=DIRECTION ( 'NONE',  ( -1.000000000000000000, 0.000000000000000000, 0.000000000000000000 ) ) ;
#2194=PLANE ( 'NONE',  #3303 ) ;
#2196=ORIENTED_EDGE ( 'NONE', *, *, #23015, .F. ) ;
#2207=FACE_BOUND ( 'NONE', #22537, .T. ) ;
#2210=EDGE_LOOP ( 'NONE', ( #23210, #13746, #15162, #12332 ) ) ;
#2229=ORIENTED_EDGE ( 'NONE', *, *, #13851, .T. ) ;
#2232=EDGE_CURVE ( 'NONE', #10767, #13127, #15521, .T. ) ;
#2233=FACE_OUTER_BOUND ( 'NONE', #21494, .T. ) ;
#2243=DIRECTION ( 'NONE',  ( -1.000000000000000000, 0.000000000000000000, 0.000000000000000000 ) ) ;
#2260=VERTEX_POINT ( 'NONE', #17564 ) ;
#2291=EDGE_CURVE ( 'NONE', #23011, #13651, #11954, .T. ) ;
#2309=LINE ( 'NONE', #13273, #15794 ) ;
#2310=ORIENTED_EDGE ( 'NONE', *, *, #11767, .F. ) ;
#2322=CARTESIAN_POINT ( 'NONE',  ( 40.23082370883257397, -29.49999999999999645, -3.000000000000000000 ) ) ;
#2325=CARTESIAN_POINT ( 'NONE',  ( -41.73082370883258108, -29.50000000000000711, -1.500000000000000000 ) ) ;
#2329=CIRCLE ( 'NONE', #14790, 10.00000000000000178 ) ;
#2343=EDGE_CURVE ( 'NONE', #20236, #19090, #10726, .T. ) ;
#2346=ORIENTED_EDGE ( 'NONE', *, *, #19695, .F. ) ;
#2358=AXIS2_PLACEMENT_3D ( 'NONE', #19430, #2707, #13442 ) ;
#2360=DIRECTION ( 'NONE',  ( -0.000000000000000000, -0.000000000000000000, 1.000000000000000000 ) ) ;
#2373=CARTESIAN_POINT ( 'NONE',  ( 0.000000000000000000, 15.50000000000000000, 14.70000000000000284 ) ) ;
#2375=EDGE_CURVE ( 'NONE', #22195, #22141, #16149, .T. ) ;
#2376=DIRECTION ( 'NONE',  ( -1.000000000000000000, 0.000000000000000000, -0.000000000000000000 ) ) ;
#2395=AXIS2_PLACEMENT_3D ( 'NONE', #18417, #23688, #16451 ) ;
#2398=AXIS2_PLACEMENT_3D ( 'NONE', #21432, #18137, #10664 ) ;
#2399=ORIENTED_EDGE ( 'NONE', *, *, #17422, .T. ) ;
#2401=EDGE_CURVE ( 'NONE', #18602, #17488, #23570, .T. ) ;
#2407=FACE_OUTER_BOUND ( 'NONE', #5414, .T. ) ;
#2408=CARTESIAN_POINT ( 'NONE',  ( -40.23082370883258108, -27.62204025492846071, -1.500000000000000000 ) ) ;
#2412=FACE_OUTER_BOUND ( 'NONE', #10329, .T. ) ;
#2418=AXIS2_PLACEMENT_3D ( 'NONE', #11978, #1037, #12232 ) ;
#2426=ADVANCED_FACE ( 'NONE', ( #5612 ), #3781, .F. ) ;
#2439=CARTESIAN_POINT ( 'NONE',  ( 29.00000000000000000, 29.50000000000000000, 14.00000000000000178 ) ) ;
#2444=VERTEX_POINT ( 'NONE', #9108 ) ;
#2459=ORIENTED_EDGE ( 'NONE', *, *, #5391, .F. ) ;
#2470=FACE_OUTER_BOUND ( 'NONE', #21015, .T. ) ;
#2491=CARTESIAN_POINT ( 'NONE',  ( -28.99999999999999645, -29.50000000000000000, -3.000000000000000000 ) ) ;
#2493=ORIENTED_EDGE ( 'NONE', *, *, #20043, .F. ) ;
#2495=TOROIDAL_SURFACE ( 'NONE', #12999, 51.49999999999999289, 1.500000000000000000 ) ;
#2504=ORIENTED_EDGE ( 'NONE', *, *, #3584, .F. ) ;
#2511=DIRECTION ( 'NONE',  ( 0.7071067811865292541, 8.659560562354708526E-17, -0.7071067811865658914 ) ) ;
#2513=DIRECTION ( 'NONE',  ( 0.7052211081716914798, -0.7089874389501491514, 0.000000000000000000 ) ) ;
#2515=DIRECTION ( 'NONE',  ( 0.000000000000000000, 0.000000000000000000, 1.000000000000000000 ) ) ;
#2517=VECTOR ( 'NONE', #18198, 1000.000000000000000 ) ;
#2519=DIRECTION ( 'NONE',  ( -0.000000000000000000, -0.000000000000000000, -1.000000000000000000 ) ) ;
#2521=AXIS2_PLACEMENT_3D ( 'NONE', #21049, #11751, #19227 ) ;
#2533=CIRCLE ( 'NONE', #20846, 4.499999999999997335 ) ;
#2544=ADVANCED_FACE ( 'NONE', ( #4236 ), #9586, .F. ) ;
#2561=ORIENTED_EDGE ( 'NONE', *, *, #13105, .F. ) ;
#2570=CARTESIAN_POINT ( 'NONE',  ( 40.00000000000000711, 15.50000000000000533, 19.20000000000000995 ) ) ;
#2579=EDGE_CURVE ( 'NONE', #17856, #5523, #4483, .T. ) ;
#2580=EDGE_CURVE ( 'NONE', #18213, #14863, #7551, .T. ) ;
#2581=AXIS2_PLACEMENT_3D ( 'NONE', #23783, #7054, #11056 ) ;
#2587=CIRCLE ( 'NONE', #12309, 40.00000000000000000 ) ;
#2593=ORIENTED_EDGE ( 'NONE', *, *, #9294, .T. ) ;
#2598=AXIS2_PLACEMENT_3D ( 'NONE', #2901, #19126, #4623 ) ;
#2601=EDGE_CURVE ( 'NONE', #2783, #10832, #4888, .T. ) ;
#2611=FACE_OUTER_BOUND ( 'NONE', #23729, .T. ) ;
#2630=DIRECTION ( 'NONE',  ( -0.000000000000000000, -0.000000000000000000, 1.000000000000000000 ) ) ;
#2634=CYLINDRICAL_SURFACE ( 'NONE', #11041, 4.249999999999996447 ) ;
#2652=EDGE_LOOP ( 'NONE', ( #11425, #21561, #18459, #15988 ) ) ;
#2654=DIRECTION ( 'NONE',  ( -1.000000000000000000, 0.000000000000000000, 0.000000000000000000 ) ) ;
#2655=EDGE_LOOP ( 'NONE', ( #10033, #1130, #15908, #23674 ) ) ;
#2656=DIRECTION ( 'NONE',  ( 1.000000000000000000, 0.000000000000000000, 0.000000000000000000 ) ) ;
#2658=AXIS2_PLACEMENT_3D ( 'NONE', #17230, #2117, #15631 ) ;
#2672=CARTESIAN_POINT ( 'NONE',  ( 42.00000000000000000, 25.22443390181681622, -3.000000000000000000 ) ) ;
#2673=VERTEX_POINT ( 'NONE', #5780 ) ;
#2683=DIRECTION ( 'NONE',  ( -1.000000000000000000, 0.000000000000000000, 0.000000000000000000 ) ) ;
#2689=DIRECTION ( 'NONE',  ( 0.000000000000000000, 0.000000000000000000, -1.000000000000000000 ) ) ;
#2691=FACE_BOUND ( 'NONE', #19838, .T. ) ;
#2707=DIRECTION ( 'NONE',  ( -0.000000000000000000, -0.000000000000000000, -1.000000000000000000 ) ) ;
#2709=EDGE_CURVE ( 'NONE', #15558, #6547, #2533, .T. ) ;
#2711=FACE_OUTER_BOUND ( 'NONE', #15416, .T. ) ;
#2712=DIRECTION ( 'NONE',  ( -1.000000000000000000, 0.000000000000000000, 0.000000000000000000 ) ) ;
#2717=CARTESIAN_POINT ( 'NONE',  ( -35.99999999999995026, 59.99999999999998579, 12.50000000000000000 ) ) ;
#2723=DIRECTION ( 'NONE',  ( 1.000000000000000000, 0.000000000000000000, -0.000000000000000000 ) ) ;
#2743=CARTESIAN_POINT ( 'NONE',  ( -30.16774287754690675, -40.66994976491903913, -1.500000000000000000 ) ) ;
#2780=CARTESIAN_POINT ( 'NONE',  ( 40.23082370883260239, 29.49999999999999645, -3.000000000000000000 ) ) ;
#2783=VERTEX_POINT ( 'NONE', #1582 ) ;
#2816=ORIENTED_EDGE ( 'NONE', *, *, #8520, .F. ) ;
#2820=CIRCLE ( 'NONE', #1655, 5.024999999999998579 ) ;
#2828=DIRECTION ( 'NONE',  ( -1.000000000000000000, 0.000000000000000000, 0.000000000000000000 ) ) ;
#2834=VERTEX_POINT ( 'NONE', #23911 ) ;
#2837=AXIS2_PLACEMENT_3D ( 'NONE', #13150, #16804, #9612 ) ;
#2841=CIRCLE ( 'NONE', #15260, 8.000000000000000000 ) ;
#2853=LINE ( 'NONE', #10025, #4504 ) ;
#2855=DIRECTION ( 'NONE',  ( 1.000000000000000000, 0.000000000000000000, 0.000000000000000000 ) ) ;
#2856=DIRECTION ( 'NONE',  ( -1.000000000000000000, 0.000000000000000000, 0.000000000000000000 ) ) ;
#2859=CONICAL_SURFACE ( 'NONE', #3637, 5.025000000000002132, 0.7853981633974482790 ) ;
#2860=ORIENTED_EDGE ( 'NONE', *, *, #22614, .T. ) ;
#2868=AXIS2_PLACEMENT_3D ( 'NONE', #7210, #14654, #18440 ) ;
#2874=VERTEX_POINT ( 'NONE', #6840 ) ;
#2876=CARTESIAN_POINT ( 'NONE',  ( 29.00000000000000355, -29.50000000000000000, -3.000000000000000000 ) ) ;
#2887=CARTESIAN_POINT ( 'NONE',  ( 3.890962118697714531E-15, 15.50000000000000000, 7.700000000000001954 ) ) ;
#2894=ORIENTED_EDGE ( 'NONE', *, *, #23368, .T. ) ;
#2897=ORIENTED_EDGE ( 'NONE', *, *, #21028, .T. ) ;
#2899=DIRECTION ( 'NONE',  ( 1.000000000000000000, 0.000000000000000000, 0.000000000000000000 ) ) ;
#2901=CARTESIAN_POINT ( 'NONE',  ( -36.00000000000000711, -51.00000000000000711, 12.50000000000000000 ) ) ;
#2903=EDGE_CURVE ( 'NONE', #15606, #12988, #4953, .T. ) ;
#2911=VECTOR ( 'NONE', #20824, 999.9999999999998863 ) ;
#2923=VECTOR ( 'NONE', #1992, 1000.000000000000000 ) ;
#2932=FACE_OUTER_BOUND ( 'NONE', #23982, .T. ) ;
#2944=CARTESIAN_POINT ( 'NONE',  ( -27.89784171216405895, -41.49349862090491570, -3.000000000000000000 ) ) ;
#2966=CIRCLE ( 'NONE', #22457, 5.000000000000004441 ) ;
#2968=AXIS2_PLACEMENT_3D ( 'NONE', #10307, #8840, #19477 ) ;
#2969=AXIS2_PLACEMENT_3D ( 'NONE', #10762, #16731, #14898 ) ;
#2973=ORIENTED_EDGE ( 'NONE', *, *, #23743, .F. ) ;
#2978=ORIENTED_EDGE ( 'NONE', *, *, #16991, .F. ) ;
#2987=ORIENTED_EDGE ( 'NONE', *, *, #20243, .T. ) ;
#3002=CARTESIAN_POINT ( 'NONE',  ( 30.68762588338046982, -45.64284848299539732, 0.000000000000000000 ) ) ;
#3003=CIRCLE ( 'NONE', #14233, 4.499999999999997335 ) ;
#3009=CIRCLE ( 'NONE', #6109, 15.00000000000000000 ) ;
#3022=VERTEX_POINT ( 'NONE', #2408 ) ;
#3028=VERTEX_POINT ( 'NONE', #11553 ) ;
#3029=VERTEX_POINT ( 'NONE', #9712 ) ;
#3035=DIRECTION ( 'NONE',  ( -0.000000000000000000, -0.000000000000000000, 1.000000000000000000 ) ) ;
#3037=CARTESIAN_POINT ( 'NONE',  ( 0.000000000000000000, 45.00000000000000000, -3.000000000000000000 ) ) ;
#3041=ORIENTED_EDGE ( 'NONE', *, *, #7196, .F. ) ;
#3045=EDGE_LOOP ( 'NONE', ( #22197, #12783, #17080, #561 ) ) ;
#3048=EDGE_LOOP ( 'NONE', ( #20407, #11966, #17754, #17029 ) ) ;
#3051=VECTOR ( 'NONE', #7490, 1000.000000000000000 ) ;
#3055=DIRECTION ( 'NONE',  ( -1.000000000000000000, -4.625929269271481378E-15, 0.000000000000000000 ) ) ;
#3064=CARTESIAN_POINT ( 'NONE',  ( -35.99999999999993605, -60.00000000000000000, 0.000000000000000000 ) ) ;
#3080=DIRECTION ( 'NONE',  ( -0.000000000000000000, -0.000000000000000000, 1.000000000000000000 ) ) ;
#3090=VERTEX_POINT ( 'NONE', #9960 ) ;
#3091=DIRECTION ( 'NONE',  ( 0.000000000000000000, 1.000000000000000000, 0.000000000000000000 ) ) ;
#3102=ADVANCED_FACE ( 'NONE', ( #17533 ), #8129, .F. ) ;
#3110=DIRECTION ( 'NONE',  ( -4.625929269271503466E-15, -1.000000000000000000, 0.000000000000000000 ) ) ;
#3129=EDGE_CURVE ( 'NONE', #13291, #10256, #7974, .T. ) ;
#3133=CYLINDRICAL_SURFACE ( 'NONE', #3317, 5.000000000000004441 ) ;
#3140=EDGE_LOOP ( 'NONE', ( #23236, #15420, #21623, #6765 ) ) ;
#3141=DIRECTION ( 'NONE',  ( -0.000000000000000000, 1.000000000000000000, 0.000000000000000000 ) ) ;
#3145=CARTESIAN_POINT ( 'NONE',  ( 33.25000000000000000, -29.50000000000000000, 12.50000000000000000 ) ) ;
#3149=ADVANCED_FACE ( 'NONE', ( #14460, #3258 ), #21924, .T. ) ;
#3151=CARTESIAN_POINT ( 'NONE',  ( -24.75000000000000000, -29.50000000000000000, -3.000000000000000000 ) ) ;
#3156=CIRCLE ( 'NONE', #12892, 39.49999999999999289 ) ;
#3167=EDGE_LOOP ( 'NONE', ( #17551, #6439, #16128, #23450 ) ) ;
#3174=ADVANCED_FACE ( 'NONE', ( #16197 ), #16303, .F. ) ;
#3177=ORIENTED_EDGE ( 'NONE', *, *, #10395, .T. ) ;
#3179=ORIENTED_EDGE ( 'NONE', *, *, #17629, .F. ) ;
#3182=DIRECTION ( 'NONE',  ( -0.000000000000000000, -0.000000000000000000, -1.000000000000000000 ) ) ;
#3184=CARTESIAN_POINT ( 'NONE',  ( 3.890962118697714531E-15, 15.50000000000000000, 7.700000000000001954 ) ) ;
#3235=ADVANCED_FACE ( 'NONE', ( #22062 ), #22416, .F. ) ;
#3240=DIRECTION ( 'NONE',  ( -0.000000000000000000, 0.000000000000000000, -1.000000000000000000 ) ) ;
#3244=AXIS2_PLACEMENT_3D ( 'NONE', #17007, #18843, #16751 ) ;
#3247=CIRCLE ( 'NONE', #7906, 2.024999999999999911 ) ;
#3248=CIRCLE ( 'NONE', #158, 49.99999999999998579 ) ;
#3258=FACE_BOUND ( 'NONE', #7345, .T. ) ;
#3261=AXIS2_PLACEMENT_3D ( 'NONE', #2127, #7365, #18610 ) ;
#3264=AXIS2_PLACEMENT_3D ( 'NONE', #2887, #814, #10317 ) ;
#3266=DIRECTION ( 'NONE',  ( -0.000000000000000000, -0.000000000000000000, -1.000000000000000000 ) ) ;
#3271=DIRECTION ( 'NONE',  ( -0.000000000000000000, -0.000000000000000000, -1.000000000000000000 ) ) ;
#3274=ORIENTED_EDGE ( 'NONE', *, *, #4287, .F. ) ;
#3281=ORIENTED_EDGE ( 'NONE', *, *, #5953, .T. ) ;
#3283=VECTOR ( 'NONE', #15723, 1000.000000000000000 ) ;
#3284=DIRECTION ( 'NONE',  ( 1.000000000000000000, 0.000000000000000000, 0.000000000000000000 ) ) ;
#3289=EDGE_CURVE ( 'NONE', #12524, #5796, #20186, .T. ) ;
#3293=DIRECTION ( 'NONE',  ( -1.000000000000000000, 0.000000000000000000, 0.000000000000000000 ) ) ;
#3298=EDGE_CURVE ( 'NONE', #13441, #18281, #3610, .T. ) ;
#3303=AXIS2_PLACEMENT_3D ( 'NONE', #13100, #11244, #13214 ) ;
#3304=CYLINDRICAL_SURFACE ( 'NONE', #13237, 4.249999999999996447 ) ;
#3312=EDGE_LOOP ( 'NONE', ( #13669, #19594, #13174 ) ) ;
#3317=AXIS2_PLACEMENT_3D ( 'NONE', #23651, #17910, #2656 ) ;
#3327=VECTOR ( 'NONE', #724, 1000.000000000000000 ) ;
#3331=AXIS2_PLACEMENT_3D ( 'NONE', #6853, #14282, #8902 ) ;
#3334=CARTESIAN_POINT ( 'NONE',  ( 30.16774287754692807, 40.66994976491903913, -1.500000000000000000 ) ) ;
#3336=ORIENTED_EDGE ( 'NONE', *, *, #9299, .T. ) ;
#3341=CARTESIAN_POINT ( 'NONE',  ( 27.99999999999998934, 50.99999999999999289, 0.000000000000000000 ) ) ;
#3343=CIRCLE ( 'NONE', #23616, 4.249999999999996447 ) ;
#3350=EDGE_CURVE ( 'NONE', #1470, #6327, #6553, .T. ) ;
#3357=LINE ( 'NONE', #10777, #15718 ) ;
#3366=CARTESIAN_POINT ( 'NONE',  ( 1.999999999999997113, -45.00000000000000000, -2.974999999999996092 ) ) ;
#3373=PRODUCT_DEFINITION_FORMATION_WITH_SPECIFIED_SOURCE ( 'ANY', '', #18223, .NOT_KNOWN. ) ;
#3377=EDGE_CURVE ( 'NONE', #17524, #11505, #13154, .T. ) ;
#3398=DIRECTION ( 'NONE',  ( 0.000000000000000000, 0.000000000000000000, -1.000000000000000000 ) ) ;
#3401=ADVANCED_FACE ( 'NONE', ( #23945 ), #1146, .F. ) ;
#3408=DIRECTION ( 'NONE',  ( 5.501724186093582121E-16, -1.000000000000000000, -0.000000000000000000 ) ) ;
#3409=DIRECTION ( 'NONE',  ( -0.000000000000000000, -0.000000000000000000, -1.000000000000000000 ) ) ;
#3413=DIRECTION ( 'NONE',  ( 0.000000000000000000, 0.000000000000000000, 1.000000000000000000 ) ) ;
#3433=CARTESIAN_POINT ( 'NONE',  ( 1.999999999999996669, -45.00000000000000000, -3.000000000000000000 ) ) ;
#3441=EDGE_LOOP ( 'NONE', ( #4211, #4386, #3915, #5619 ) ) ;
#3444=CIRCLE ( 'NONE', #23334, 1.500000000000001332 ) ;
#3446=ORIENTED_EDGE ( 'NONE', *, *, #7255, .F. ) ;
#3449=CARTESIAN_POINT ( 'NONE',  ( 42.00000000000000000, 25.22443390181681622, -1.500000000000000000 ) ) ;
#3454=DIRECTION ( 'NONE',  ( -1.000000000000000000, 0.000000000000000000, 0.000000000000000000 ) ) ;
#3456=CARTESIAN_POINT ( 'NONE',  ( 0.000000000000000000, -45.00000000000000000, -3.000000000000000000 ) ) ;
#3469=LINE ( 'NONE', #19947, #15749 ) ;
#3471=CARTESIAN_POINT ( 'NONE',  ( -43.50000000000000711, 25.84341543330624091, 0.000000000000000000 ) ) ;
#3472=CARTESIAN_POINT ( 'NONE',  ( -9.999999999999998224, 15.50000000000000178, -40.80000000000000426 ) ) ;
#3476=FACE_OUTER_BOUND ( 'NONE', #19992, .T. ) ;
#3481=ADVANCED_FACE ( 'NONE', ( #10562 ), #11035, .F. ) ;
#3525=DIRECTION ( 'NONE',  ( -0.000000000000000000, -0.000000000000000000, 1.000000000000000000 ) ) ;
#3529=ORIENTED_EDGE ( 'NONE', *, *, #5774, .F. ) ;
#3533=CARTESIAN_POINT ( 'NONE',  ( -28.99999999999999645, 29.50000000000000711, -1.500000000000000000 ) ) ;
#3538=EDGE_CURVE ( 'NONE', #13580, #12511, #3444, .T. ) ;
#3540=VERTEX_POINT ( 'NONE', #14593 ) ;
#3552=LINE ( 'NONE', #1612, #6431 ) ;
#3557=DIRECTION ( 'NONE',  ( -0.000000000000000000, 0.000000000000000000, -1.000000000000000000 ) ) ;
#3558=DIRECTION ( 'NONE',  ( -0.000000000000000000, -0.000000000000000000, -1.000000000000000000 ) ) ;
#3559=AXIS2_PLACEMENT_3D ( 'NONE', #18340, #23614, #20183 ) ;
#3561=CARTESIAN_POINT ( 'NONE',  ( -28.00000000000000355, -51.00000000000000711, 0.5000000000000000000 ) ) ;
#3571=DIRECTION ( 'NONE',  ( -0.000000000000000000, -0.000000000000000000, 1.000000000000000000 ) ) ;
#3576=AXIS2_PLACEMENT_3D ( 'NONE', #11920, #13639, #7653 ) ;
#3577=EDGE_CURVE ( 'NONE', #21069, #2444, #19035, .T. ) ;
#3581=ORIENTED_EDGE ( 'NONE', *, *, #6763, .F. ) ;
#3584=EDGE_CURVE ( 'NONE', #15649, #16325, #9268, .T. ) ;
#3587=DIRECTION ( 'NONE',  ( -0.000000000000000000, -0.000000000000000000, 1.000000000000000000 ) ) ;
#3600=VECTOR ( 'NONE', #4184, 1000.000000000000000 ) ;
#3609=LINE ( 'NONE', #18862, #16227 ) ;
#3610=LINE ( 'NONE', #18508, #3051 ) ;
#3615=CARTESIAN_POINT ( 'NONE',  ( 44.99999999999998579, -51.00000000000000711, 12.50000000000000000 ) ) ;
#3626=DIRECTION ( 'NONE',  ( 0.8298699724180977899, -0.5579568342432823513, 0.000000000000000000 ) ) ;
#3637=AXIS2_PLACEMENT_3D ( 'NONE', #2876, #1295, #10171 ) ;
#3638=AXIS2_PLACEMENT_3D ( 'NONE', #15712, #12161, #17806 ) ;
#3643=AXIS2_PLACEMENT_3D ( 'NONE', #541, #7961, #13590 ) ;
#3644=CARTESIAN_POINT ( 'NONE',  ( 35.99999999999999289, -51.00000000000000711, 0.5000000000000000000 ) ) ;
#3651=VERTEX_POINT ( 'NONE', #7986 ) ;
#3652=FACE_OUTER_BOUND ( 'NONE', #16888, .T. ) ;
#3655=CARTESIAN_POINT ( 'NONE',  ( -36.00000000000000711, -51.00000000000000711, 0.5000000000000000000 ) ) ;
#3659=DIRECTION ( 'NONE',  ( -1.000000000000000000, 0.000000000000000000, 0.000000000000000000 ) ) ;
#3660=EDGE_LOOP ( 'NONE', ( #549, #11280, #19293, #10654 ) ) ;
#3667=ORIENTED_EDGE ( 'NONE', *, *, #7536, .T. ) ;
#3681=ORIENTED_EDGE ( 'NONE', *, *, #11214, .F. ) ;
#3691=CARTESIAN_POINT ( 'NONE',  ( -42.38288618805137276, -26.96649534593477426, 0.000000000000000000 ) ) ;
#3693=CARTESIAN_POINT ( 'NONE',  ( 44.99999999999998579, -51.00000000000000711, 0.000000000000000000 ) ) ;
#3694=CARTESIAN_POINT ( 'NONE',  ( -41.73082370883257397, -27.62204025492845361, -1.500000000000000000 ) ) ;
#3706=CARTESIAN_POINT ( 'NONE',  ( 30.68762588338046982, -45.64284848299539732, -3.000000000000000000 ) ) ;
#3710=AXIS2_PLACEMENT_3D ( 'NONE', #10334, #19864, #5207 ) ;
#3714=DIRECTION ( 'NONE',  ( -1.000000000000000000, 0.000000000000000000, 0.000000000000000000 ) ) ;
#3715=ORIENTED_EDGE ( 'NONE', *, *, #9732, .T. ) ;
#3716=DIRECTION ( 'NONE',  ( -1.000000000000000000, 0.000000000000000000, 0.000000000000000000 ) ) ;
#3719=CYLINDRICAL_SURFACE ( 'NONE', #16961, 49.99999999999998579 ) ;
#3722=LINE ( 'NONE', #3952, #9862 ) ;
#3723=CARTESIAN_POINT ( 'NONE',  ( -1.999999999999996669, 45.00000000000000000, -8.673617379884035472E-16 ) ) ;
#3726=VECTOR ( 'NONE', #21552, 1000.000000000000000 ) ;
#3728=ORIENTED_EDGE ( 'NONE', *, *, #19908, .T. ) ;
#3731=ADVANCED_FACE ( 'NONE', ( #13730 ), #11755, .F. ) ;
#3739=DIRECTION ( 'NONE',  ( 0.000000000000000000, 0.000000000000000000, -1.000000000000000000 ) ) ;
#3748=DIRECTION ( 'NONE',  ( -1.000000000000000000, 0.000000000000000000, 0.000000000000000000 ) ) ;
#3752=CARTESIAN_POINT ( 'NONE',  ( -42.00000000000000000, 25.22443390181683043, -1.500000000000000000 ) ) ;
#3764=EDGE_CURVE ( 'NONE', #3090, #16565, #4715, .T. ) ;
#3770=DIRECTION ( 'NONE',  ( -1.000000000000000000, 0.000000000000000000, 0.000000000000000000 ) ) ;
#3771=CARTESIAN_POINT ( 'NONE',  ( 40.23082370883260239, 27.62204025492844650, -3.000000000000000000 ) ) ;
#3775=EDGE_LOOP ( 'NONE', ( #9540, #21194, #22865, #2504 ) ) ;
#3781=CYLINDRICAL_SURFACE ( 'NONE', #11432, 8.000000000000000000 ) ;
#3789=ORIENTED_EDGE ( 'NONE', *, *, #22915, .F. ) ;
#3793=ORIENTED_EDGE ( 'NONE', *, *, #7425, .T. ) ;
#3794=CARTESIAN_POINT ( 'NONE',  ( 0.000000000000000000, 0.000000000000000000, 0.000000000000000000 ) ) ;
#3796=DIRECTION ( 'NONE',  ( -1.000000000000000000, -0.000000000000000000, -0.000000000000000000 ) ) ;
#3797=LINE ( 'NONE', #10358, #7520 ) ;
#3800=PLANE ( 'NONE',  #13430 ) ;
#3804=ADVANCED_FACE ( 'NONE', ( #15808 ), #14385, .F. ) ;
#3806=FACE_OUTER_BOUND ( 'NONE', #16811, .T. ) ;
#3823=EDGE_LOOP ( 'NONE', ( #1028, #20674, #15851, #5881 ) ) ;
#3828=CIRCLE ( 'NONE', #21766, 4.249999999999996447 ) ;
#3847=CLOSED_SHELL ( 'NONE', ( #21423, #3174, #14767, #13187, #8286, #4679, #21159, #17566, #12323, #17976, #7985, #13752, #10821, #1816, #7327, #18525, #23038, #10281, #1535, #8413, #3804, #10791, #7223, #9782, #23463, #19552, #6576, #17550, #21702, #14865, #7168, #11415, #17068, #9235, #8943, #6069, #5441, #4126, #6178, #10336, #14481, #22171, #23191, #1659, #5327, #5725, #3149, #16986, #17232, #18784, #4191, #17763, #8442, #10782, #10359, #13638, #6441, #3235, #18818, #21830, #20365, #10471, #14537, #14980, #1229, #11476, #8648, #2544, #16056, #7053, #5948, #10010, #9327, #6955, #19076, #14662, #4189, #4201, #217, #3731, #14080, #22731, #8646, #18471, #11086, #12825, #14591, #14304, #6334, #7226, #705, #9992, #3102, #12888, #6959, #17749, #13786, #16402, #5597, #13612, #14574, #15390, #1934, #20135, #21094, #2426, #6713, #11844, #4331, #9818, #23923, #3401, #19809, #961, #6496, #4281, #9176, #3481, #22547, #17213, #12583, #14317, #9248, #20517, #18565, #8743, #15583 ) ) ;
#3858=CARTESIAN_POINT ( 'NONE',  ( -40.66734255040739043, 26.56420859267092283, -1.500000000000000000 ) ) ;
#3859=CARTESIAN_POINT ( 'NONE',  ( 3.890962118697714531E-15, 15.50000000000000000, 19.20000000000000995 ) ) ;
#3862=EDGE_CURVE ( 'NONE', #18287, #10867, #18869, .T. ) ;
#3865=CARTESIAN_POINT ( 'NONE',  ( -42.62132034355964549, 25.48082444701821103, -1.614108343103369153E-16 ) ) ;
#3886=EDGE_CURVE ( 'NONE', #5851, #14876, #3469, .T. ) ;
#3896=DIRECTION ( 'NONE',  ( -0.000000000000000000, -0.000000000000000000, -1.000000000000000000 ) ) ;
#3908=DIRECTION ( 'NONE',  ( 1.000000000000000000, 0.000000000000000000, 0.000000000000000000 ) ) ;
#3915=ORIENTED_EDGE ( 'NONE', *, *, #21862, .T. ) ;
#3921=FACE_OUTER_BOUND ( 'NONE', #2652, .T. ) ;
#3924=FACE_OUTER_BOUND ( 'NONE', #10986, .T. ) ;
#3930=ORIENTED_EDGE ( 'NONE', *, *, #2375, .F. ) ;
#3941=EDGE_CURVE ( 'NONE', #20601, #5111, #2109, .T. ) ;
#3944=VECTOR ( 'NONE', #15602, 1000.000000000000000 ) ;
#3945=ORIENTED_EDGE ( 'NONE', *, *, #22475, .T. ) ;
#3947=FACE_OUTER_BOUND ( 'NONE', #23258, .T. ) ;
#3951=EDGE_LOOP ( 'NONE', ( #7215, #10549, #3281, #7774 ) ) ;
#3952=CARTESIAN_POINT ( 'NONE',  ( -40.66734255040739043, 26.56420859267092283, -3.000000000000000000 ) ) ;
#3954=CARTESIAN_POINT ( 'NONE',  ( 31.49999999999999289, -51.00000000000000711, 12.50000000000000000 ) ) ;
#3955=ORIENTED_EDGE ( 'NONE', *, *, #11637, .F. ) ;
#3961=AXIS2_PLACEMENT_3D ( 'NONE', #7767, #9841, #2182 ) ;
#3971=EDGE_CURVE ( 'NONE', #2260, #10767, #20931, .T. ) ;
#3979=CARTESIAN_POINT ( 'NONE',  ( 28.99999999999998579, -29.49999999999999645, 0.000000000000000000 ) ) ;
#3999=VECTOR ( 'NONE', #18027, 1000.000000000000000 ) ;
#4011=CARTESIAN_POINT ( 'NONE',  ( 29.00000000000000000, 29.50000000000000000, 14.00000000000000178 ) ) ;
#4014=APPLICATION_CONTEXT ( 'automotive_design' ) ;
#4036=FACE_OUTER_BOUND ( 'NONE', #18575, .T. ) ;
#4045=CIRCLE ( 'NONE', #19239, 4.499999999999997335 ) ;
#4050=CIRCLE ( 'NONE', #20808, 8.000000000000000000 ) ;
#4053=DIRECTION ( 'NONE',  ( -0.000000000000000000, -0.000000000000000000, 1.000000000000000000 ) ) ;
#4055=ORIENTED_EDGE ( 'NONE', *, *, #13933, .F. ) ;
#4062=EDGE_CURVE ( 'NONE', #4924, #5717, #11609, .T. ) ;
#4073=ORIENTED_EDGE ( 'NONE', *, *, #2401, .F. ) ;
#4074=CIRCLE ( 'NONE', #200, 8.000000000000000000 ) ;
#4086=EDGE_LOOP ( 'NONE', ( #17233, #2987, #16759, #1176 ) ) ;
#4093=AXIS2_PLACEMENT_3D ( 'NONE', #22674, #20861, #8018 ) ;
#4104=ORIENTED_EDGE ( 'NONE', *, *, #9021, .F. ) ;
#4118=CIRCLE ( 'NONE', #3331, 4.249999999999996447 ) ;
#4125=EDGE_CURVE ( 'NONE', #13623, #3029, #3828, .T. ) ;
#4126=ADVANCED_FACE ( 'NONE', ( #12966 ), #13324, .T. ) ;
#4127=VECTOR ( 'NONE', #18758, 1000.000000000000000 ) ;
#4128=ORIENTED_EDGE ( 'NONE', *, *, #9507, .F. ) ;
#4141=ORIENTED_EDGE ( 'NONE', *, *, #1211, .T. ) ;
#4142=CARTESIAN_POINT ( 'NONE',  ( -36.00000000000000711, -51.00000000000000711, 12.50000000000000000 ) ) ;
#4148=CYLINDRICAL_SURFACE ( 'NONE', #2837, 4.249999999999996447 ) ;
#4150=EDGE_CURVE ( 'NONE', #23011, #12230, #6019, .T. ) ;
#4156=AXIS2_PLACEMENT_3D ( 'NONE', #15889, #6373, #2712 ) ;
#4161=EDGE_CURVE ( 'NONE', #13291, #8450, #19829, .T. ) ;
#4162=ORIENTED_EDGE ( 'NONE', *, *, #5391, .T. ) ;
#4163=EDGE_CURVE ( 'NONE', #17900, #11505, #21773, .T. ) ;
#4168=AXIS2_PLACEMENT_3D ( 'NONE', #3706, #3571, #2107 ) ;
#4183=AXIS2_PLACEMENT_3D ( 'NONE', #6242, #21126, #2828 ) ;
#4184=DIRECTION ( 'NONE',  ( -0.000000000000000000, -1.000000000000000000, -0.000000000000000000 ) ) ;
#4189=ADVANCED_FACE ( 'NONE', ( #12087 ), #5374, .F. ) ;
#4191=ADVANCED_FACE ( 'NONE', ( #19561 ), #896, .T. ) ;
#4201=ADVANCED_FACE ( 'NONE', ( #15900 ), #9901, .F. ) ;
#4202=EDGE_LOOP ( 'NONE', ( #14797, #11093 ) ) ;
#4207=VERTEX_POINT ( 'NONE', #662 ) ;
#4209=DIRECTION ( 'NONE',  ( -1.000000000000000000, 0.000000000000000000, 0.000000000000000000 ) ) ;
#4211=ORIENTED_EDGE ( 'NONE', *, *, #4125, .F. ) ;
#4218=ORIENTED_EDGE ( 'NONE', *, *, #15134, .F. ) ;
#4222=FACE_OUTER_BOUND ( 'NONE', #14254, .T. ) ;
#4236=FACE_OUTER_BOUND ( 'NONE', #23387, .T. ) ;
#4252=FACE_OUTER_BOUND ( 'NONE', #4086, .T. ) ;
#4271=VERTEX_POINT ( 'NONE', #15516 ) ;
#4279=FACE_OUTER_BOUND ( 'NONE', #1390, .T. ) ;
#4281=ADVANCED_FACE ( 'NONE', ( #2611, #17476 ), #4571, .F. ) ;
#4287=EDGE_CURVE ( 'NONE', #1878, #18602, #10136, .T. ) ;
#4288=EDGE_CURVE ( 'NONE', #7451, #21069, #559, .T. ) ;
#4297=LINE ( 'NONE', #19425, #3600 ) ;
#4304=DIRECTION ( 'NONE',  ( 0.000000000000000000, 0.000000000000000000, -1.000000000000000000 ) ) ;
#4306=ORIENTED_EDGE ( 'NONE', *, *, #11333, .T. ) ;
#4309=CARTESIAN_POINT ( 'NONE',  ( 40.00000000000000711, 15.50000000000000533, 12.50000000000000000 ) ) ;
#4318=CARTESIAN_POINT ( 'NONE',  ( 41.73082370883260239, 29.49999999999999645, 0.000000000000000000 ) ) ;
#4322=ORIENTED_EDGE ( 'NONE', *, *, #11637, .T. ) ;
#4325=CARTESIAN_POINT ( 'NONE',  ( -31.50000000000000711, -51.00000000000000711, 0.5000000000000004441 ) ) ;
#4331=ADVANCED_FACE ( 'NONE', ( #7980, #4222 ), #20449, .T. ) ;
#4341=DIRECTION ( 'NONE',  ( -0.000000000000000000, -0.000000000000000000, 1.000000000000000000 ) ) ;
#4350=CYLINDRICAL_SURFACE ( 'NONE', #23233, 1.500000000000000000 ) ;
#4354=CARTESIAN_POINT ( 'NONE',  ( -40.23082370883260239, 29.50000000000000711, -3.000000000000000000 ) ) ;
#4365=DIRECTION ( 'NONE',  ( 0.000000000000000000, 0.000000000000000000, 1.000000000000000000 ) ) ;
#4368=CARTESIAN_POINT ( 'NONE',  ( 35.99999999999992184, -60.00000000000000000, 12.50000000000000000 ) ) ;
#4386=ORIENTED_EDGE ( 'NONE', *, *, #16386, .T. ) ;
#4411=ORIENTED_EDGE ( 'NONE', *, *, #12173, .T. ) ;
#4414=CARTESIAN_POINT ( 'NONE',  ( 0.000000000000000000, 45.00000000000000000, -3.000000000000000000 ) ) ;
#4416=CIRCLE ( 'NONE', #6357, 5.025000000000002132 ) ;
#4442=ORIENTED_EDGE ( 'NONE', *, *, #15884, .T. ) ;
#4446=DIRECTION ( 'NONE',  ( -0.000000000000000000, -0.000000000000000000, -1.000000000000000000 ) ) ;
#4451=CARTESIAN_POINT ( 'NONE',  ( -44.00000000000001421, 50.99999999999999289, 0.5000000000000000000 ) ) ;
#4454=ORIENTED_EDGE ( 'NONE', *, *, #15224, .T. ) ;
#4468=AXIS2_PLACEMENT_3D ( 'NONE', #839, #14248, #4638 ) ;
#4480=ORIENTED_EDGE ( 'NONE', *, *, #14219, .T. ) ;
#4482=FACE_OUTER_BOUND ( 'NONE', #9215, .T. ) ;
#4483=CIRCLE ( 'NONE', #18114, 1.499999999999994449 ) ;
#4484=AXIS2_PLACEMENT_3D ( 'NONE', #11306, #16593, #23925 ) ;
#4486=ORIENTED_EDGE ( 'NONE', *, *, #2232, .F. ) ;
#4492=CARTESIAN_POINT ( 'NONE',  ( 41.73082370883257397, 50.99999999999999289, 0.000000000000000000 ) ) ;
#4503=( NAMED_UNIT ( * ) PLANE_ANGLE_UNIT ( ) SI_UNIT ( $, .RADIAN. ) );
#4504=VECTOR ( 'NONE', #17370, 1000.000000000000000 ) ;
#4517=AXIS2_PLACEMENT_3D ( 'NONE', #3037, #19630, #6929 ) ;
#4550=EDGE_CURVE ( 'NONE', #5717, #18213, #13388, .T. ) ;
#4552=EDGE_CURVE ( 'NONE', #10649, #12205, #21186, .T. ) ;
#4563=DIRECTION ( 'NONE',  ( -0.000000000000000000, -0.000000000000000000, -1.000000000000000000 ) ) ;
#4565=AXIS2_PLACEMENT_3D ( 'NONE', #6953, #5113, #14376 ) ;
#4570=ORIENTED_EDGE ( 'NONE', *, *, #20979, .T. ) ;
#4571=PLANE ( 'NONE',  #550 ) ;
#4584=DIRECTION ( 'NONE',  ( -1.000000000000000000, 0.000000000000000000, 0.000000000000000000 ) ) ;
#4586=CARTESIAN_POINT ( 'NONE',  ( 27.99999999999998934, -51.00000000000000711, 0.000000000000000000 ) ) ;
#4587=DIRECTION ( 'NONE',  ( -0.000000000000000000, -0.000000000000000000, -1.000000000000000000 ) ) ;
#4606=VERTEX_POINT ( 'NONE', #21665 ) ;
#4607=CARTESIAN_POINT ( 'NONE',  ( 27.89784171216406961, 41.49349862090490859, -3.000000000000000000 ) ) ;
#4614=ORIENTED_EDGE ( 'NONE', *, *, #17666, .F. ) ;
#4623=DIRECTION ( 'NONE',  ( -1.000000000000000000, 0.000000000000000000, 0.000000000000000000 ) ) ;
#4638=DIRECTION ( 'NONE',  ( 1.000000000000000000, 0.000000000000000000, 0.000000000000000000 ) ) ;
#4651=DIRECTION ( 'NONE',  ( 1.000000000000000000, 0.000000000000000000, 0.000000000000000000 ) ) ;
#4662=DIRECTION ( 'NONE',  ( -0.000000000000000000, -0.000000000000000000, 1.000000000000000000 ) ) ;
#4675=EDGE_CURVE ( 'NONE', #18344, #10068, #3797, .T. ) ;
#4677=EDGE_CURVE ( 'NONE', #21210, #4271, #10645, .T. ) ;
#4679=ADVANCED_FACE ( 'NONE', ( #2711 ), #22776, .F. ) ;
#4685=DIRECTION ( 'NONE',  ( 0.000000000000000000, 1.000000000000000000, 0.000000000000000000 ) ) ;
#4691=DIRECTION ( 'NONE',  ( -1.000000000000000000, -0.000000000000000000, -0.000000000000000000 ) ) ;
#4704=ORIENTED_EDGE ( 'NONE', *, *, #21763, .T. ) ;
#4705=VERTEX_POINT ( 'NONE', #10009 ) ;
#4707=DIRECTION ( 'NONE',  ( -0.000000000000000000, -0.000000000000000000, 1.000000000000000000 ) ) ;
#4715=LINE ( 'NONE', #1175, #21803 ) ;
#4716=ORIENTED_EDGE ( 'NONE', *, *, #19691, .F. ) ;
#4724=DIRECTION ( 'NONE',  ( -1.000000000000000000, 0.000000000000000000, 0.000000000000000000 ) ) ;
#4732=ORIENTED_EDGE ( 'NONE', *, *, #2343, .T. ) ;
#4754=LINE ( 'NONE', #7037, #4794 ) ;
#4765=CARTESIAN_POINT ( 'NONE',  ( -36.00000000000001421, 50.99999999999999289, 0.5000000000000000000 ) ) ;
#4787=ORIENTED_EDGE ( 'NONE', *, *, #247, .F. ) ;
#4790=ORIENTED_EDGE ( 'NONE', *, *, #6630, .T. ) ;
#4794=VECTOR ( 'NONE', #14467, 1000.000000000000000 ) ;
#4795=CIRCLE ( 'NONE', #18413, 11.23082370883260062 ) ;
#4797=VECTOR ( 'NONE', #8329, 1000.000000000000000 ) ;
#4806=VERTEX_POINT ( 'NONE', #18779 ) ;
#4807=DIRECTION ( 'NONE',  ( -0.000000000000000000, -0.000000000000000000, 1.000000000000000000 ) ) ;
#4808=EDGE_LOOP ( 'NONE', ( #9400, #10254 ) ) ;
#4823=DIRECTION ( 'NONE',  ( -1.000000000000000000, 0.000000000000000000, 0.000000000000000000 ) ) ;
#4833=AXIS2_PLACEMENT_3D ( 'NONE', #8871, #4882, #16312 ) ;
#4834=CONICAL_SURFACE ( 'NONE', #17272, 39.49999999999999289, 0.7853981633974621568 ) ;
#4845=FACE_OUTER_BOUND ( 'NONE', #15467, .T. ) ;
#4848=CARTESIAN_POINT ( 'NONE',  ( 41.99999999999997158, -25.22443390181681622, -1.500000000000000000 ) ) ;
#4849=CARTESIAN_POINT ( 'NONE',  ( -1.999999999999997113, 45.00000000000000000, -2.974999999999996092 ) ) ;
#4852=LINE ( 'NONE', #17777, #18539 ) ;
#4863=VERTEX_POINT ( 'NONE', #7424 ) ;
#4874=VECTOR ( 'NONE', #18326, 1000.000000000000000 ) ;
#4879=CARTESIAN_POINT ( 'NONE',  ( -43.49999999999997868, -25.84341543330624091, 0.000000000000000000 ) ) ;
#4882=DIRECTION ( 'NONE',  ( -0.000000000000000000, -0.000000000000000000, 1.000000000000000000 ) ) ;
#4888=CIRCLE ( 'NONE', #5651, 15.00000000000000000 ) ;
#4901=CARTESIAN_POINT ( 'NONE',  ( -24.75000000000000000, -29.50000000000000000, 12.50000000000000000 ) ) ;
#4914=CIRCLE ( 'NONE', #8403, 39.49999999999999289 ) ;
#4917=EDGE_CURVE ( 'NONE', #3022, #6856, #7938, .T. ) ;
#4919=CIRCLE ( 'NONE', #2157, 15.00000000000000000 ) ;
#4924=VERTEX_POINT ( 'NONE', #8147 ) ;
#4932=ORIENTED_EDGE ( 'NONE', *, *, #21763, .F. ) ;
#4941=EDGE_CURVE ( 'NONE', #14876, #15606, #6217, .T. ) ;
#4942=DIRECTION ( 'NONE',  ( -0.000000000000000000, -0.000000000000000000, 1.000000000000000000 ) ) ;
#4953=CIRCLE ( 'NONE', #8027, 4.250000000000000000 ) ;
#4958=CARTESIAN_POINT ( 'NONE',  ( 34.02499999999999858, 29.50000000000000000, -3.000000000000000000 ) ) ;
#4975=CARTESIAN_POINT ( 'NONE',  ( 41.73082370883260239, 50.99999999999999289, 0.000000000000000000 ) ) ;
#4993=VERTEX_POINT ( 'NONE', #19150 ) ;
#4996=ORIENTED_EDGE ( 'NONE', *, *, #5507, .F. ) ;
#5020=EDGE_CURVE ( 'NONE', #1863, #1766, #15754, .T. ) ;
#5023=ORIENTED_EDGE ( 'NONE', *, *, #16836, .F. ) ;
#5028=AXIS2_PLACEMENT_3D ( 'NONE', #20281, #11098, #14535 ) ;
#5029=DIRECTION ( 'NONE',  ( 0.000000000000000000, 0.000000000000000000, -1.000000000000000000 ) ) ;
#5035=DIRECTION ( 'NONE',  ( -0.000000000000000000, -0.000000000000000000, -1.000000000000000000 ) ) ;
#5037=ORIENTED_EDGE ( 'NONE', *, *, #16308, .T. ) ;
#5040=CYLINDRICAL_SURFACE ( 'NONE', #8252, 15.00000000000000000 ) ;
#5041=DIRECTION ( 'NONE',  ( -0.000000000000000000, -0.000000000000000000, -1.000000000000000000 ) ) ;
#5055=CARTESIAN_POINT ( 'NONE',  ( -41.99999999999997158, -25.22443390181683043, -3.000000000000000000 ) ) ;
#5064=CARTESIAN_POINT ( 'NONE',  ( 3.890962118697714531E-15, 15.50000000000000000, 7.700000000000001954 ) ) ;
#5068=DIRECTION ( 'NONE',  ( 1.000000000000000000, -4.625929269271481378E-15, 0.000000000000000000 ) ) ;
#5075=AXIS2_PLACEMENT_3D ( 'NONE', #17703, #10246, #21252 ) ;
#5103=EDGE_CURVE ( 'NONE', #8450, #15532, #6824, .T. ) ;
#5111=VERTEX_POINT ( 'NONE', #16115 ) ;
#5112=CARTESIAN_POINT ( 'NONE',  ( 28.99999999999998579, -29.49999999999999645, -3.000000000000000000 ) ) ;
#5113=DIRECTION ( 'NONE',  ( -0.000000000000000000, -0.000000000000000000, -1.000000000000000000 ) ) ;
#5114=CARTESIAN_POINT ( 'NONE',  ( 0.000000000000000000, 0.000000000000000000, -3.000000000000000000 ) ) ;
#5120=EDGE_LOOP ( 'NONE', ( #15275, #22815, #12477, #5023 ) ) ;
#5128=EDGE_LOOP ( 'NONE', ( #20065, #6190 ) ) ;
#5159=DIRECTION ( 'NONE',  ( -0.000000000000000000, -0.000000000000000000, -1.000000000000000000 ) ) ;
#5163=CARTESIAN_POINT ( 'NONE',  ( -29.00000000000000000, 29.50000000000000000, 16.55365763086713216 ) ) ;
#5169=ORIENTED_EDGE ( 'NONE', *, *, #12371, .T. ) ;
#5189=DIRECTION ( 'NONE',  ( 0.7052211081716904806, 0.7089874389501500396, 0.000000000000000000 ) ) ;
#5193=EDGE_CURVE ( 'NONE', #11499, #11436, #20063, .T. ) ;
#5202=DIRECTION ( 'NONE',  ( 0.000000000000000000, 0.000000000000000000, 1.000000000000000000 ) ) ;
#5207=DIRECTION ( 'NONE',  ( 1.000000000000000000, 0.000000000000000000, -0.000000000000000000 ) ) ;
#5211=CIRCLE ( 'NONE', #23531, 3.500000000000003109 ) ;
#5212=DIRECTION ( 'NONE',  ( -0.7071067811865474617, 0.000000000000000000, -0.7071067811865474617 ) ) ;
#5219=CARTESIAN_POINT ( 'NONE',  ( -14.99999999999999645, 15.50000000000000178, 7.700000000000001954 ) ) ;
#5221=CARTESIAN_POINT ( 'NONE',  ( -42.00000000000000000, 25.22443390181683043, -3.000000000000000000 ) ) ;
#5243=AXIS2_PLACEMENT_3D ( 'NONE', #1530, #10775, #18240 ) ;
#5245=CIRCLE ( 'NONE', #17710, 4.499999999999997335 ) ;
#5259=CARTESIAN_POINT ( 'NONE',  ( -45.00000000000001421, 50.99999999999992184, 12.50000000000000000 ) ) ;
#5270=DIRECTION ( 'NONE',  ( 0.000000000000000000, 0.000000000000000000, 1.000000000000000000 ) ) ;
#5273=DIRECTION ( 'NONE',  ( 0.7052211081716915908, -0.7089874389501490404, 0.000000000000000000 ) ) ;
#5282=CIRCLE ( 'NONE', #18915, 4.499999999999997335 ) ;
#5283=DIRECTION ( 'NONE',  ( -1.000000000000000000, 0.000000000000000000, 0.000000000000000000 ) ) ;
#5286=ORIENTED_EDGE ( 'NONE', *, *, #23686, .T. ) ;
#5292=CARTESIAN_POINT ( 'NONE',  ( 3.890962118697714531E-15, 15.50000000000000000, -2.999999999999999112 ) ) ;
#5296=CONICAL_SURFACE ( 'NONE', #16959, 2.024999999999999911, 0.7853981633974222998 ) ;
#5303=CARTESIAN_POINT ( 'NONE',  ( 3.890962118697714531E-15, 15.50000000000000000, 7.700000000000001954 ) ) ;
#5319=CARTESIAN_POINT ( 'NONE',  ( -45.00000000000001421, 50.99999999999992184, 12.50000000000000000 ) ) ;
#5327=ADVANCED_FACE ( 'NONE', ( #18911 ), #2194, .F. ) ;
#5331=ORIENTED_EDGE ( 'NONE', *, *, #2709, .F. ) ;
#5334=TOROIDAL_SURFACE ( 'NONE', #23983, 51.49999999999999289, 1.500000000000000000 ) ;
#5336=CARTESIAN_POINT ( 'NONE',  ( -39.99999999999999289, 15.50000000000000000, 19.20000000000000995 ) ) ;
#5347=ORIENTED_EDGE ( 'NONE', *, *, #7304, .F. ) ;
#5358=ORIENTED_EDGE ( 'NONE', *, *, #12429, .F. ) ;
#5374=TOROIDAL_SURFACE ( 'NONE', #19011, 12.73082370883260062, 1.500000000000000000 ) ;
#5376=DIRECTION ( 'NONE',  ( -1.000000000000000000, 0.000000000000000000, 0.000000000000000000 ) ) ;
#5391=EDGE_CURVE ( 'NONE', #21092, #6327, #8360, .T. ) ;
#5393=DIRECTION ( 'NONE',  ( 0.000000000000000000, 0.000000000000000000, -1.000000000000000000 ) ) ;
#5414=EDGE_LOOP ( 'NONE', ( #7539, #18217, #20096, #15248 ) ) ;
#5417=ORIENTED_EDGE ( 'NONE', *, *, #23762, .T. ) ;
#5423=CARTESIAN_POINT ( 'NONE',  ( 42.00000000000000000, 25.22443390181681622, -3.000000000000000000 ) ) ;
#5425=ORIENTED_EDGE ( 'NONE', *, *, #4287, .T. ) ;
#5430=DIRECTION ( 'NONE',  ( -0.000000000000000000, -0.000000000000000000, -1.000000000000000000 ) ) ;
#5431=EDGE_CURVE ( 'NONE', #11173, #15649, #5901, .T. ) ;
#5434=CARTESIAN_POINT ( 'NONE',  ( -1.999999999999996669, -45.00000000000000000, -8.673617379884035472E-16 ) ) ;
#5435=EDGE_CURVE ( 'NONE', #5851, #17470, #5541, .T. ) ;
#5441=ADVANCED_FACE ( 'NONE', ( #1774, #417, #9413, #18483, #9203, #7363 ), #2123, .T. ) ;
#5445=ORIENTED_EDGE ( 'NONE', *, *, #8108, .T. ) ;
#5473=EDGE_LOOP ( 'NONE', ( #5880, #8960, #19584, #10040 ) ) ;
#5486=CARTESIAN_POINT ( 'NONE',  ( 29.00000000000000000, 29.50000000000000000, -3.000000000000000000 ) ) ;
#5487=DIRECTION ( 'NONE',  ( -0.8571673007021120005, 0.000000000000000000, -0.5150380749100547106 ) ) ;
#5491=CARTESIAN_POINT ( 'NONE',  ( -36.00000000000000711, -51.00000000000000711, 12.50000000000000000 ) ) ;
#5492=DIRECTION ( 'NONE',  ( -1.000000000000000000, 0.000000000000000000, 0.000000000000000000 ) ) ;
#5495=EDGE_CURVE ( 'NONE', #22890, #20318, #13962, .T. ) ;
#5498=DIRECTION ( 'NONE',  ( -0.000000000000000000, -0.000000000000000000, -1.000000000000000000 ) ) ;
#5502=ORIENTED_EDGE ( 'NONE', *, *, #17877, .T. ) ;
#5507=EDGE_CURVE ( 'NONE', #2834, #7627, #15782, .T. ) ;
#5510=DIRECTION ( 'NONE',  ( -1.000000000000000000, 0.000000000000000000, 0.000000000000000000 ) ) ;
#5517=CIRCLE ( 'NONE', #21103, 1.499999999999998002 ) ;
#5521=EDGE_LOOP ( 'NONE', ( #21574, #11368 ) ) ;
#5523=VERTEX_POINT ( 'NONE', #19451 ) ;
#5530=AXIS2_PLACEMENT_3D ( 'NONE', #15737, #23199, #7786 ) ;
#5536=CIRCLE ( 'NONE', #11352, 40.00000000000000000 ) ;
#5540=PLANE ( 'NONE',  #15394 ) ;
#5541=LINE ( 'NONE', #11498, #2923 ) ;
#5548=AXIS2_PLACEMENT_3D ( 'NONE', #2018, #7990, #5811 ) ;
#5553=CIRCLE ( 'NONE', #12947, 10.00000000000000533 ) ;
#5564=CARTESIAN_POINT ( 'NONE',  ( 3.890962118697714531E-15, 15.50000000000000000, -40.80000000000000426 ) ) ;
#5565=VERTEX_POINT ( 'NONE', #21286 ) ;
#5570=EDGE_CURVE ( 'NONE', #13580, #13312, #22412, .T. ) ;
#5572=EDGE_CURVE ( 'NONE', #4271, #2673, #2853, .T. ) ;
#5576=DIRECTION ( 'NONE',  ( -1.000000000000000000, 0.000000000000000000, 0.000000000000000000 ) ) ;
#5577=DIRECTION ( 'NONE',  ( -1.000000000000000000, 0.000000000000000000, 0.000000000000000000 ) ) ;
#5578=VECTOR ( 'NONE', #9213, 1000.000000000000000 ) ;
#5580=DIRECTION ( 'NONE',  ( -1.000000000000000000, 0.000000000000000000, 0.000000000000000000 ) ) ;
#5590=CARTESIAN_POINT ( 'NONE',  ( 41.73082370883260239, 29.49999999999999645, -1.500000000000000000 ) ) ;
#5597=ADVANCED_FACE ( 'NONE', ( #17484 ), #12985, .F. ) ;
#5603=CIRCLE ( 'NONE', #17276, 5.000000000000004441 ) ;
#5604=VECTOR ( 'NONE', #3035, 1000.000000000000000 ) ;
#5612=FACE_OUTER_BOUND ( 'NONE', #3048, .T. ) ;
#5619=ORIENTED_EDGE ( 'NONE', *, *, #15232, .F. ) ;
#5621=AXIS2_PLACEMENT_3D ( 'NONE', #13592, #17602, #2855 ) ;
#5627=CONICAL_SURFACE ( 'NONE', #18104, 2.024999999999999911, 0.7853981633974222998 ) ;
#5633=VERTEX_POINT ( 'NONE', #17238 ) ;
#5636=CARTESIAN_POINT ( 'NONE',  ( -43.49999999999997868, -25.84341543330624091, 0.000000000000000000 ) ) ;
#5638=EDGE_CURVE ( 'NONE', #16665, #15653, #1703, .T. ) ;
#5651=AXIS2_PLACEMENT_3D ( 'NONE', #1916, #2024, #20589 ) ;
#5668=EDGE_CURVE ( 'NONE', #21092, #16520, #21187, .T. ) ;
#5676=CIRCLE ( 'NONE', #21658, 17.25000000000000000 ) ;
#5717=VERTEX_POINT ( 'NONE', #20177 ) ;
#5725=ADVANCED_FACE ( 'NONE', ( #16015 ), #23719, .T. ) ;
#5754=FACE_OUTER_BOUND ( 'NONE', #13457, .T. ) ;
#5756=ORIENTED_EDGE ( 'NONE', *, *, #15832, .F. ) ;
#5760=CARTESIAN_POINT ( 'NONE',  ( 35.99999999999999289, 50.99999999999999289, 0.5000000000000000000 ) ) ;
#5764=CARTESIAN_POINT ( 'NONE',  ( 0.000000000000000000, 32.75000000000000000, 14.70000000000000284 ) ) ;
#5767=DIRECTION ( 'NONE',  ( -1.000000000000000000, 0.000000000000000000, 0.000000000000000000 ) ) ;
#5768=ORIENTED_EDGE ( 'NONE', *, *, #14299, .T. ) ;
#5769=DIRECTION ( 'NONE',  ( -0.000000000000000000, -0.000000000000000000, -1.000000000000000000 ) ) ;
#5774=EDGE_CURVE ( 'NONE', #2874, #10068, #3247, .T. ) ;
#5780=CARTESIAN_POINT ( 'NONE',  ( -28.00000000000001066, 50.99999999999999289, 0.000000000000000000 ) ) ;
#5785=ORIENTED_EDGE ( 'NONE', *, *, #23042, .T. ) ;
#5792=CARTESIAN_POINT ( 'NONE',  ( 35.99999999999999289, -51.00000000000000711, 12.50000000000000000 ) ) ;
#5796=VERTEX_POINT ( 'NONE', #1401 ) ;
#5799=VERTEX_POINT ( 'NONE', #286 ) ;
#5805=FACE_OUTER_BOUND ( 'NONE', #8558, .T. ) ;
#5810=EDGE_LOOP ( 'NONE', ( #22785, #11840 ) ) ;
#5811=DIRECTION ( 'NONE',  ( -1.000000000000000000, 0.000000000000000000, 0.000000000000000000 ) ) ;
#5815=DIRECTION ( 'NONE',  ( -0.7089874389501527041, 0.7052211081716879271, 0.000000000000000000 ) ) ;
#5820=( NAMED_UNIT ( * ) SI_UNIT ( $, .STERADIAN. ) SOLID_ANGLE_UNIT ( ) );
#5824=EDGE_CURVE ( 'NONE', #15940, #47, #7566, .T. ) ;
#5828=ORIENTED_EDGE ( 'NONE', *, *, #17877, .F. ) ;
#5833=DIRECTION ( 'NONE',  ( -1.000000000000000000, 0.000000000000000000, 0.000000000000000000 ) ) ;
#5839=DIRECTION ( 'NONE',  ( -1.000000000000000000, 0.000000000000000000, 0.000000000000000000 ) ) ;
#5845=EDGE_CURVE ( 'NONE', #10567, #20508, #1328, .T. ) ;
#5851=VERTEX_POINT ( 'NONE', #1862 ) ;
#5858=CARTESIAN_POINT ( 'NONE',  ( 35.99999999999999289, 50.99999999999999289, 12.50000000000000000 ) ) ;
#5863=ORIENTED_EDGE ( 'NONE', *, *, #15730, .T. ) ;
#5876=DIRECTION ( 'NONE',  ( -1.000000000000000000, 0.000000000000000000, 0.000000000000000000 ) ) ;
#5880=ORIENTED_EDGE ( 'NONE', *, *, #9299, .F. ) ;
#5881=ORIENTED_EDGE ( 'NONE', *, *, #23632, .T. ) ;
#5888=EDGE_LOOP ( 'NONE', ( #11999, #24043, #88, #8112 ) ) ;
#5900=DIRECTION ( 'NONE',  ( -0.000000000000000000, -0.000000000000000000, -1.000000000000000000 ) ) ;
#5901=LINE ( 'NONE', #18715, #8745 ) ;
#5904=FACE_OUTER_BOUND ( 'NONE', #16920, .T. ) ;
#5918=EDGE_CURVE ( 'NONE', #12230, #15766, #13183, .T. ) ;
#5924=VERTEX_POINT ( 'NONE', #20642 ) ;
#5930=DIRECTION ( 'NONE',  ( -0.000000000000000000, -0.000000000000000000, -1.000000000000000000 ) ) ;
#5934=VECTOR ( 'NONE', #18273, 1000.000000000000000 ) ;
#5936=DIRECTION ( 'NONE',  ( -1.000000000000000000, 0.000000000000000000, 0.000000000000000000 ) ) ;
#5947=UNCERTAINTY_MEASURE_WITH_UNIT (LENGTH_MEASURE( 1.000000000000000082E-05 ), #13251, 'distance_accuracy_value', 'NONE');
#5948=ADVANCED_FACE ( 'NONE', ( #3476 ), #18713, .F. ) ;
#5950=CYLINDRICAL_SURFACE ( 'NONE', #15807, 4.249999999999996447 ) ;
#5953=EDGE_CURVE ( 'NONE', #16325, #12105, #17001, .T. ) ;
#5954=VERTEX_POINT ( 'NONE', #15040 ) ;
#5962=CIRCLE ( 'NONE', #13747, 4.499999999999997335 ) ;
#5967=AXIS2_PLACEMENT_3D ( 'NONE', #11202, #5498, #18677 ) ;
#5970=VERTEX_POINT ( 'NONE', #22510 ) ;
#5972=ORIENTED_EDGE ( 'NONE', *, *, #18094, .T. ) ;
#5977=ORIENTED_EDGE ( 'NONE', *, *, #23194, .T. ) ;
#5978=CARTESIAN_POINT ( 'NONE',  ( 0.000000000000000000, 0.000000000000000000, 0.000000000000000000 ) ) ;
#5984=DIRECTION ( 'NONE',  ( 0.000000000000000000, 0.000000000000000000, 1.000000000000000000 ) ) ;
#5985=EDGE_CURVE ( 'NONE', #12105, #22724, #5536, .T. ) ;
#5991=CARTESIAN_POINT ( 'NONE',  ( -36.00000000000000711, -51.00000000000000711, 0.000000000000000000 ) ) ;
#5994=AXIS2_PLACEMENT_3D ( 'NONE', #11749, #19225, #18793 ) ;
#6002=CIRCLE ( 'NONE', #21213, 1.499999999999998002 ) ;
#6013=ORIENTED_EDGE ( 'NONE', *, *, #13933, .T. ) ;
#6019=LINE ( 'NONE', #24080, #8101 ) ;
#6031=FACE_OUTER_BOUND ( 'NONE', #7266, .T. ) ;
#6033=ORIENTED_EDGE ( 'NONE', *, *, #9294, .F. ) ;
#6038=EDGE_LOOP ( 'NONE', ( #15422, #9736, #22539, #23478 ) ) ;
#6039=AXIS2_PLACEMENT_3D ( 'NONE', #12795, #16335, #9133 ) ;
#6053=CARTESIAN_POINT ( 'NONE',  ( -28.99999999999999645, -29.50000000000000000, -3.000000000000000000 ) ) ;
#6056=TOROIDAL_SURFACE ( 'NONE', #19712, 12.73082370883260772, 1.500000000000000000 ) ;
#6057=ORIENTED_EDGE ( 'NONE', *, *, #19185, .T. ) ;
#6058=FACE_OUTER_BOUND ( 'NONE', #3823, .T. ) ;
#6065=CIRCLE ( 'NONE', #19716, 4.249999999999996447 ) ;
#6069=ADVANCED_FACE ( 'NONE', ( #20310, #20667, #12972, #3947, #18481, #11131, #2120, #18606 ), #305, .F. ) ;
#6096=ORIENTED_EDGE ( 'NONE', *, *, #16375, .F. ) ;
#6097=VERTEX_POINT ( 'NONE', #23245 ) ;
#6104=ORIENTED_EDGE ( 'NONE', *, *, #16386, .F. ) ;
#6106=EDGE_CURVE ( 'NONE', #21210, #6921, #13698, .T. ) ;
#6108=CARTESIAN_POINT ( 'NONE',  ( -10.00000000000000355, 15.50000000000000178, -2.999999999999999112 ) ) ;
#6109=AXIS2_PLACEMENT_3D ( 'NONE', #12425, #21952, #10827 ) ;
#6112=CARTESIAN_POINT ( 'NONE',  ( -27.89784171216405895, 41.49349862090491570, -3.000000000000000000 ) ) ;
#6133=EDGE_CURVE ( 'NONE', #10152, #22249, #10141, .T. ) ;
#6139=VERTEX_POINT ( 'NONE', #539 ) ;
#6140=VERTEX_POINT ( 'NONE', #4318 ) ;
#6152=CARTESIAN_POINT ( 'NONE',  ( -34.02499999999999858, 29.50000000000000000, -3.000000000000000000 ) ) ;
#6160=ORIENTED_EDGE ( 'NONE', *, *, #22266, .T. ) ;
#6163=LINE ( 'NONE', #685, #18439 ) ;
#6165=CARTESIAN_POINT ( 'NONE',  ( -33.24999999999999289, 29.50000000000000000, 14.00000000000000178 ) ) ;
#6174=VERTEX_POINT ( 'NONE', #8074 ) ;
#6177=DIRECTION ( 'NONE',  ( -0.000000000000000000, 1.000000000000000000, -0.000000000000000000 ) ) ;
#6178=ADVANCED_FACE ( 'NONE', ( #17236 ), #21031, .F. ) ;
#6190=ORIENTED_EDGE ( 'NONE', *, *, #19217, .F. ) ;
#6192=ORIENTED_EDGE ( 'NONE', *, *, #12726, .F. ) ;
#6195=ORIENTED_EDGE ( 'NONE', *, *, #6133, .F. ) ;
#6198=CARTESIAN_POINT ( 'NONE',  ( -35.99999999999993605, -60.00000000000000000, 12.50000000000000000 ) ) ;
#6202=FACE_OUTER_BOUND ( 'NONE', #16718, .T. ) ;
#6204=CARTESIAN_POINT ( 'NONE',  ( 3.890962118697714531E-15, 15.50000000000000000, 19.70000000000000284 ) ) ;
#6206=DIRECTION ( 'NONE',  ( 0.000000000000000000, -1.000000000000000000, 0.000000000000000000 ) ) ;
#6207=DIRECTION ( 'NONE',  ( -1.000000000000000000, 0.000000000000000000, 0.000000000000000000 ) ) ;
#6217=LINE ( 'NONE', #17684, #3283 ) ;
#6219=CARTESIAN_POINT ( 'NONE',  ( 35.99999999999999289, 50.99999999999999289, 12.50000000000000000 ) ) ;
#6223=PLANE ( 'NONE',  #5530 ) ;
#6226=ORIENTED_EDGE ( 'NONE', *, *, #4917, .F. ) ;
#6233=EDGE_CURVE ( 'NONE', #1549, #11505, #21765, .T. ) ;
#6242=CARTESIAN_POINT ( 'NONE',  ( 29.00000000000000000, 29.50000000000000000, -2.224999999999995204 ) ) ;
#6255=EDGE_LOOP ( 'NONE', ( #14576, #287, #13685 ) ) ;
#6263=DIRECTION ( 'NONE',  ( -0.000000000000000000, -0.000000000000000000, -1.000000000000000000 ) ) ;
#6264=CARTESIAN_POINT ( 'NONE',  ( 3.890962118697714531E-15, 15.50000000000000000, 12.50000000000000000 ) ) ;
#6269=ORIENTED_EDGE ( 'NONE', *, *, #19806, .F. ) ;
#6276=EDGE_CURVE ( 'NONE', #14424, #6139, #19571, .T. ) ;
#6286=EDGE_LOOP ( 'NONE', ( #8917, #5972, #8327, #21855 ) ) ;
#6289=ORIENTED_EDGE ( 'NONE', *, *, #16306, .F. ) ;
#6290=DIRECTION ( 'NONE',  ( 0.000000000000000000, 0.000000000000000000, -1.000000000000000000 ) ) ;
#6291=CARTESIAN_POINT ( 'NONE',  ( -28.99999999999999645, -29.50000000000000000, -3.000000000000000000 ) ) ;
#6297=ORIENTED_EDGE ( 'NONE', *, *, #11164, .T. ) ;
#6302=SHAPE_REPRESENTATION_RELATIONSHIP ( 'NONE' , 'NONE' ,  #1013, #10480 ) ;
#6312=CARTESIAN_POINT ( 'NONE',  ( -42.62132034355961707, -25.48082444701823235, -4.874844804309807125E-16 ) ) ;
#6317=DIRECTION ( 'NONE',  ( -1.000000000000000000, 0.000000000000000000, 0.000000000000000000 ) ) ;
#6327=VERTEX_POINT ( 'NONE', #3334 ) ;
#6328=ORIENTED_EDGE ( 'NONE', *, *, #2601, .F. ) ;
#6334=ADVANCED_FACE ( 'NONE', ( #8461 ), #23369, .F. ) ;
#6357=AXIS2_PLACEMENT_3D ( 'NONE', #8358, #1064, #21429 ) ;
#6363=CARTESIAN_POINT ( 'NONE',  ( 24.75000000000000000, 29.50000000000000000, -2.224999999999995204 ) ) ;
#6373=DIRECTION ( 'NONE',  ( 0.000000000000000000, 0.000000000000000000, -1.000000000000000000 ) ) ;
#6379=EDGE_CURVE ( 'NONE', #12712, #17488, #14667, .T. ) ;
#6380=AXIS2_PLACEMENT_3D ( 'NONE', #1619, #18457, #1400 ) ;
#6395=CARTESIAN_POINT ( 'NONE',  ( -36.00000000000000711, -51.00000000000000711, 12.50000000000000000 ) ) ;
#6398=DIRECTION ( 'NONE',  ( -0.7071067811865574537, 0.000000000000000000, -0.7071067811865376918 ) ) ;
#6410=CIRCLE ( 'NONE', #2521, 4.249999999999996447 ) ;
#6412=ORIENTED_EDGE ( 'NONE', *, *, #22227, .F. ) ;
#6431=VECTOR ( 'NONE', #10966, 1000.000000000000000 ) ;
#6439=ORIENTED_EDGE ( 'NONE', *, *, #12129, .F. ) ;
#6441=ADVANCED_FACE ( 'NONE', ( #31 ), #16837, .F. ) ;
#6442=ORIENTED_EDGE ( 'NONE', *, *, #8739, .F. ) ;
#6448=CARTESIAN_POINT ( 'NONE',  ( 44.99999999999998579, -51.00000000000000711, 12.50000000000000000 ) ) ;
#6456=CARTESIAN_POINT ( 'NONE',  ( -40.23082370883260239, 29.50000000000000711, -1.500000000000000000 ) ) ;
#6465=CIRCLE ( 'NONE', #18535, 1.500000000000000000 ) ;
#6480=CARTESIAN_POINT ( 'NONE',  ( 33.25000000000000000, -29.50000000000000000, -3.000000000000000000 ) ) ;
#6481=AXIS2_PLACEMENT_3D ( 'NONE', #22284, #22532, #18735 ) ;
#6492=DIRECTION ( 'NONE',  ( 1.000000000000000000, 0.000000000000000000, 0.000000000000000000 ) ) ;
#6496=ADVANCED_FACE ( 'NONE', ( #3806, #22489 ), #9168, .F. ) ;
#6505=DIRECTION ( 'NONE',  ( -1.000000000000000000, 0.000000000000000000, -0.000000000000000000 ) ) ;
#6529=CARTESIAN_POINT ( 'NONE',  ( -28.99999999999999645, 29.50000000000000711, 0.000000000000000000 ) ) ;
#6531=DIRECTION ( 'NONE',  ( -1.000000000000000000, 0.000000000000000000, 0.000000000000000000 ) ) ;
#6535=EDGE_LOOP ( 'NONE', ( #19906, #24062, #20460, #14143 ) ) ;
#6547=VERTEX_POINT ( 'NONE', #10116 ) ;
#6553=CIRCLE ( 'NONE', #18233, 5.000000000000000888 ) ;
#6554=DIRECTION ( 'NONE',  ( -0.7071067811865443531, 0.000000000000000000, -0.7071067811865506814 ) ) ;
#6566=DIRECTION ( 'NONE',  ( -0.000000000000000000, -0.000000000000000000, -1.000000000000000000 ) ) ;
#6567=EDGE_LOOP ( 'NONE', ( #17799, #9493, #11772, #7121 ) ) ;
#6571=CIRCLE ( 'NONE', #5028, 8.999999999999994671 ) ;
#6572=CARTESIAN_POINT ( 'NONE',  ( 40.23082370883260239, 29.49999999999999645, -1.500000000000000000 ) ) ;
#6576=ADVANCED_FACE ( 'NONE', ( #7796 ), #20759, .F. ) ;
#6580=VECTOR ( 'NONE', #11708, 1000.000000000000000 ) ;
#6581=ORIENTED_EDGE ( 'NONE', *, *, #14880, .F. ) ;
#6587=ORIENTED_EDGE ( 'NONE', *, *, #5507, .T. ) ;
#6597=FACE_OUTER_BOUND ( 'NONE', #20772, .T. ) ;
#6598=CARTESIAN_POINT ( 'NONE',  ( 35.99999999999999289, 50.99999999999999289, 0.5000000000000004441 ) ) ;
#6615=VECTOR ( 'NONE', #21113, 1000.000000000000000 ) ;
#6628=CARTESIAN_POINT ( 'NONE',  ( 23.97500000000000497, -29.50000000000000000, -3.000000000000000000 ) ) ;
#6630=EDGE_CURVE ( 'NONE', #3540, #13580, #4297, .T. ) ;
#6638=CARTESIAN_POINT ( 'NONE',  ( -41.73082370883257397, -27.62204025492845361, -1.500000000000000000 ) ) ;
#6640=CARTESIAN_POINT ( 'NONE',  ( 35.99999999999992184, 59.99999999999998579, 12.50000000000000000 ) ) ;
#6651=DIRECTION ( 'NONE',  ( 0.7071067811865443531, 8.659560562354894648E-17, -0.7071067811865506814 ) ) ;
#6659=CARTESIAN_POINT ( 'NONE',  ( 41.73082370883260239, 29.49999999999999645, -1.500000000000000000 ) ) ;
#6665=CARTESIAN_POINT ( 'NONE',  ( -40.23082370883260239, 27.62204025492846071, -3.000000000000000000 ) ) ;
#6674=LINE ( 'NONE', #14106, #6580 ) ;
#6682=FACE_OUTER_BOUND ( 'NONE', #22147, .T. ) ;
#6689=EDGE_CURVE ( 'NONE', #15771, #13623, #20344, .T. ) ;
#6696=CARTESIAN_POINT ( 'NONE',  ( -30.68762588338046982, -45.64284848299540442, -1.500000000000000000 ) ) ;
#6701=ORIENTED_EDGE ( 'NONE', *, *, #20818, .T. ) ;
#6702=ORIENTED_EDGE ( 'NONE', *, *, #17522, .F. ) ;
#6706=CARTESIAN_POINT ( 'NONE',  ( 35.99999999999999289, -51.00000000000000711, 0.000000000000000000 ) ) ;
#6713=ADVANCED_FACE ( 'NONE', ( #1339, #21942 ), #23773, .T. ) ;
#6716=LINE ( 'NONE', #21611, #21909 ) ;
#6739=CARTESIAN_POINT ( 'NONE',  ( -30.16774287754690675, -40.66994976491903913, -3.000000000000000000 ) ) ;
#6755=DIRECTION ( 'NONE',  ( -1.000000000000000000, 0.000000000000000000, 0.000000000000000000 ) ) ;
#6763=EDGE_CURVE ( 'NONE', #12230, #4924, #23884, .T. ) ;
#6765=ORIENTED_EDGE ( 'NONE', *, *, #15502, .F. ) ;
#6790=CIRCLE ( 'NONE', #5621, 4.499999999999997335 ) ;
#6791=CYLINDRICAL_SURFACE ( 'NONE', #7903, 1.499999999999998002 ) ;
#6821=ORIENTED_EDGE ( 'NONE', *, *, #11164, .F. ) ;
#6824=CIRCLE ( 'NONE', #17719, 5.000000000000004441 ) ;
#6831=AXIS2_PLACEMENT_3D ( 'NONE', #9336, #9453, #5936 ) ;
#6832=ORIENTED_EDGE ( 'NONE', *, *, #14383, .F. ) ;
#6840=CARTESIAN_POINT ( 'NONE',  ( 2.024999999999999911, -45.00000000000000000, -3.000000000000000000 ) ) ;
#6841=DIRECTION ( 'NONE',  ( -1.000000000000000000, 0.000000000000000000, 0.000000000000000000 ) ) ;
#6853=CARTESIAN_POINT ( 'NONE',  ( 29.00000000000000355, -29.50000000000000000, 12.50000000000000000 ) ) ;
#6856=VERTEX_POINT ( 'NONE', #7858 ) ;
#6863=CARTESIAN_POINT ( 'NONE',  ( -40.66734255040736201, -26.56420859267092283, -3.000000000000000000 ) ) ;
#6865=VECTOR ( 'NONE', #4807, 1000.000000000000000 ) ;
#6867=ORIENTED_EDGE ( 'NONE', *, *, #2903, .F. ) ;
#6869=AXIS2_PLACEMENT_3D ( 'NONE', #5114, #23433, #12534 ) ;
#6873=ORIENTED_EDGE ( 'NONE', *, *, #16121, .F. ) ;
#6877=DIRECTION ( 'NONE',  ( 0.000000000000000000, 0.000000000000000000, 1.000000000000000000 ) ) ;
#6896=CARTESIAN_POINT ( 'NONE',  ( -23.97499999999999787, 29.50000000000000000, -3.000000000000000000 ) ) ;
#6900=DIRECTION ( 'NONE',  ( -1.000000000000000000, 0.000000000000000000, 0.000000000000000000 ) ) ;
#6908=EDGE_CURVE ( 'NONE', #16103, #10767, #9234, .T. ) ;
#6921=VERTEX_POINT ( 'NONE', #7750 ) ;
#6929=DIRECTION ( 'NONE',  ( -1.000000000000000000, 0.000000000000000000, 0.000000000000000000 ) ) ;
#6936=DIRECTION ( 'NONE',  ( -1.000000000000000000, 0.000000000000000000, 0.000000000000000000 ) ) ;
#6937=ORIENTED_EDGE ( 'NONE', *, *, #15576, .T. ) ;
#6942=VERTEX_POINT ( 'NONE', #16045 ) ;
#6946=ORIENTED_EDGE ( 'NONE', *, *, #20515, .F. ) ;
#6953=CARTESIAN_POINT ( 'NONE',  ( -30.68762588338048403, 45.64284848299540442, -1.500000000000000000 ) ) ;
#6955=ADVANCED_FACE ( 'NONE', ( #7016 ), #1186, .F. ) ;
#6959=ADVANCED_FACE ( 'NONE', ( #9075 ), #6791, .F. ) ;
#6965=CARTESIAN_POINT ( 'NONE',  ( -45.00000000000000000, -50.99999999999993605, 12.50000000000000000 ) ) ;
#6967=DIRECTION ( 'NONE',  ( -0.000000000000000000, -0.000000000000000000, -1.000000000000000000 ) ) ;
#6990=DIRECTION ( 'NONE',  ( -0.000000000000000000, -0.000000000000000000, 1.000000000000000000 ) ) ;
#6993=EDGE_LOOP ( 'NONE', ( #481, #2561, #11154, #4480 ) ) ;
#7012=CARTESIAN_POINT ( 'NONE',  ( 28.99999999999999645, 29.49999999999999645, -1.500000000000000000 ) ) ;
#7016=FACE_OUTER_BOUND ( 'NONE', #9821, .T. ) ;
#7017=CARTESIAN_POINT ( 'NONE',  ( -1.999999999999996669, 45.00000000000000000, -3.000000000000000000 ) ) ;
#7019=FACE_OUTER_BOUND ( 'NONE', #23269, .T. ) ;
#7029=CARTESIAN_POINT ( 'NONE',  ( -42.00000000000000000, 25.22443390181683043, -3.000000000000000000 ) ) ;
#7037=CARTESIAN_POINT ( 'NONE',  ( 27.99999999999998934, -51.00000000000000711, 0.5000000000000000000 ) ) ;
#7052=LINE ( 'NONE', #14483, #20704 ) ;
#7053=ADVANCED_FACE ( 'NONE', ( #5904 ), #7718, .F. ) ;
#7054=DIRECTION ( 'NONE',  ( -0.000000000000000000, -0.000000000000000000, -1.000000000000000000 ) ) ;
#7057=CYLINDRICAL_SURFACE ( 'NONE', #16838, 8.000000000000000000 ) ;
#7059=CONICAL_SURFACE ( 'NONE', #11315, 5.024999999999998579, 0.7853981633974438381 ) ;
#7061=LINE ( 'NONE', #23791, #7576 ) ;
#7072=DIRECTION ( 'NONE',  ( -1.000000000000000000, -8.326672684688666165E-15, 0.000000000000000000 ) ) ;
#7082=EDGE_CURVE ( 'NONE', #16520, #1470, #138, .T. ) ;
#7087=CARTESIAN_POINT ( 'NONE',  ( -14.99999999999999645, 15.50000000000000178, 7.700000000000001954 ) ) ;
#7103=DIRECTION ( 'NONE',  ( -1.000000000000000000, 0.000000000000000000, 0.000000000000000000 ) ) ;
#7104=ORIENTED_EDGE ( 'NONE', *, *, #16836, .T. ) ;
#7105=CIRCLE ( 'NONE', #14495, 4.499999999999997335 ) ;
#7107=CARTESIAN_POINT ( 'NONE',  ( -41.73082370883257397, -27.62204025492845361, -1.500000000000000000 ) ) ;
#7111=VERTEX_POINT ( 'NONE', #20565 ) ;
#7121=ORIENTED_EDGE ( 'NONE', *, *, #19695, .T. ) ;
#7127=LINE ( 'NONE', #3472, #20765 ) ;
#7146=ORIENTED_EDGE ( 'NONE', *, *, #3862, .F. ) ;
#7147=ORIENTED_EDGE ( 'NONE', *, *, #5020, .T. ) ;
#7168=ADVANCED_FACE ( 'NONE', ( #9556 ), #18485, .F. ) ;
#7176=VERTEX_POINT ( 'NONE', #3723 ) ;
#7191=DIRECTION ( 'NONE',  ( -1.000000000000000000, 0.000000000000000000, 0.000000000000000000 ) ) ;
#7192=DIRECTION ( 'NONE',  ( 0.000000000000000000, 0.000000000000000000, -1.000000000000000000 ) ) ;
#7196=EDGE_CURVE ( 'NONE', #13441, #2834, #4045, .T. ) ;
#7210=CARTESIAN_POINT ( 'NONE',  ( 0.000000000000000000, 0.000000000000000000, -1.500000000000000000 ) ) ;
#7215=ORIENTED_EDGE ( 'NONE', *, *, #22597, .F. ) ;
#7219=CARTESIAN_POINT ( 'NONE',  ( -41.73082370883257397, -27.62204025492845361, -3.000000000000000000 ) ) ;
#7223=ADVANCED_FACE ( 'NONE', ( #17241 ), #15412, .F. ) ;
#7226=ADVANCED_FACE ( 'NONE', ( #17742 ), #18076, .F. ) ;
#7229=DIRECTION ( 'NONE',  ( -5.501724186093582121E-16, 1.000000000000000000, 0.000000000000000000 ) ) ;
#7246=EDGE_CURVE ( 'NONE', #10822, #3540, #9467, .T. ) ;
#7255=EDGE_CURVE ( 'NONE', #17900, #10822, #5211, .T. ) ;
#7262=CARTESIAN_POINT ( 'NONE',  ( -40.66734255040738333, 26.56420859267091927, -1.500000000000000000 ) ) ;
#7264=ORIENTED_EDGE ( 'NONE', *, *, #17125, .T. ) ;
#7266=EDGE_LOOP ( 'NONE', ( #890, #6587, #22467, #11541 ) ) ;
#7273=CARTESIAN_POINT ( 'NONE',  ( -34.02499999999999858, -29.50000000000000000, -3.000000000000000000 ) ) ;
#7275=CIRCLE ( 'NONE', #19715, 4.249999999999996447 ) ;
#7289=CARTESIAN_POINT ( 'NONE',  ( -36.00000000000000711, -51.00000000000000711, 0.5000000000000000000 ) ) ;
#7295=EDGE_LOOP ( 'NONE', ( #21390, #19438, #22307, #9700 ) ) ;
#7298=DIRECTION ( 'NONE',  ( -1.000000000000000000, 0.000000000000000000, 0.000000000000000000 ) ) ;
#7303=CARTESIAN_POINT ( 'NONE',  ( 27.89784171216407316, -41.49349862090490149, -3.000000000000000000 ) ) ;
#7304=EDGE_CURVE ( 'NONE', #17812, #20236, #20927, .T. ) ;
#7310=DIRECTION ( 'NONE',  ( -0.000000000000000000, -0.000000000000000000, -1.000000000000000000 ) ) ;
#7311=DIRECTION ( 'NONE',  ( -1.000000000000000000, 0.000000000000000000, 0.000000000000000000 ) ) ;
#7316=CARTESIAN_POINT ( 'NONE',  ( -35.99999999999995026, 59.99999999999998579, 0.000000000000000000 ) ) ;
#7322=VERTEX_POINT ( 'NONE', #6152 ) ;
#7323=FACE_OUTER_BOUND ( 'NONE', #20702, .T. ) ;
#7327=ADVANCED_FACE ( 'NONE', ( #23252 ), #15785, .F. ) ;
#7345=EDGE_LOOP ( 'NONE', ( #6328, #11255 ) ) ;
#7363=FACE_OUTER_BOUND ( 'NONE', #19145, .T. ) ;
#7365=DIRECTION ( 'NONE',  ( -0.000000000000000000, -0.000000000000000000, -1.000000000000000000 ) ) ;
#7372=CIRCLE ( 'NONE', #15553, 4.499999999999997335 ) ;
#7380=ORIENTED_EDGE ( 'NONE', *, *, #16476, .F. ) ;
#7388=VECTOR ( 'NONE', #20372, 1000.000000000000000 ) ;
#7391=CARTESIAN_POINT ( 'NONE',  ( -43.50000000000000711, 25.84341543330624091, 0.000000000000000000 ) ) ;
#7396=ORIENTED_EDGE ( 'NONE', *, *, #4062, .F. ) ;
#7405=DIRECTION ( 'NONE',  ( 0.000000000000000000, 0.000000000000000000, -1.000000000000000000 ) ) ;
#7413=VECTOR ( 'NONE', #17151, 1000.000000000000000 ) ;
#7417=ORIENTED_EDGE ( 'NONE', *, *, #3377, .F. ) ;
#7424=CARTESIAN_POINT ( 'NONE',  ( -28.00000000000000355, -51.00000000000000711, 0.000000000000000000 ) ) ;
#7425=EDGE_CURVE ( 'NONE', #11436, #11499, #5553, .T. ) ;
#7438=EDGE_CURVE ( 'NONE', #18281, #7627, #7105, .T. ) ;
#7439=DIRECTION ( 'NONE',  ( 1.000000000000000000, 5.501724186093582121E-16, 0.000000000000000000 ) ) ;
#7450=EDGE_LOOP ( 'NONE', ( #16809, #20799, #21158, #15601 ) ) ;
#7451=VERTEX_POINT ( 'NONE', #5163 ) ;
#7459=CONICAL_SURFACE ( 'NONE', #21124, 4.249999999999993783, 1.029744258676653645 ) ;
#7469=EDGE_CURVE ( 'NONE', #3022, #978, #16824, .T. ) ;
#7477=CIRCLE ( 'NONE', #20358, 1.999999999999997113 ) ;
#7480=AXIS2_PLACEMENT_3D ( 'NONE', #14364, #10919, #14606 ) ;
#7483=ORIENTED_EDGE ( 'NONE', *, *, #15884, .F. ) ;
#7490=DIRECTION ( 'NONE',  ( -0.000000000000000000, -0.000000000000000000, -1.000000000000000000 ) ) ;
#7493=CARTESIAN_POINT ( 'NONE',  ( -34.02499999999999858, 29.50000000000000000, -3.000000000000000000 ) ) ;
#7494=EDGE_CURVE ( 'NONE', #4993, #6097, #20180, .T. ) ;
#7504=AXIS2_PLACEMENT_3D ( 'NONE', #18353, #12740, #1644 ) ;
#7514=ORIENTED_EDGE ( 'NONE', *, *, #23632, .F. ) ;
#7520=VECTOR ( 'NONE', #23321, 999.9999999999998863 ) ;
#7536=EDGE_CURVE ( 'NONE', #5717, #13291, #19971, .T. ) ;
#7539=ORIENTED_EDGE ( 'NONE', *, *, #18738, .T. ) ;
#7551=CIRCLE ( 'NONE', #17718, 12.73082370883259884 ) ;
#7566=LINE ( 'NONE', #7687, #18829 ) ;
#7568=CARTESIAN_POINT ( 'NONE',  ( -31.50000000000001421, 50.99999999999999289, 0.5000000000000004441 ) ) ;
#7570=CARTESIAN_POINT ( 'NONE',  ( -39.49999999999998579, 15.50000000000000000, 19.70000000000000284 ) ) ;
#7574=VECTOR ( 'NONE', #16750, 1000.000000000000000 ) ;
#7576=VECTOR ( 'NONE', #22103, 1000.000000000000000 ) ;
#7593=CARTESIAN_POINT ( 'NONE',  ( -39.99999999999999289, 15.50000000000000000, 19.70000000000000284 ) ) ;
#7607=EDGE_LOOP ( 'NONE', ( #4104, #14723, #19034, #17922 ) ) ;
#7624=ORIENTED_EDGE ( 'NONE', *, *, #5435, .T. ) ;
#7625=CONICAL_SURFACE ( 'NONE', #8026, 5.025000000000002132, 0.7853981633974482790 ) ;
#7627=VERTEX_POINT ( 'NONE', #9051 ) ;
#7636=ORIENTED_EDGE ( 'NONE', *, *, #8035, .F. ) ;
#7638=ORIENTED_EDGE ( 'NONE', *, *, #15134, .T. ) ;
#7641=CIRCLE ( 'NONE', #22478, 8.000000000000000000 ) ;
#7653=DIRECTION ( 'NONE',  ( -1.000000000000000000, 0.000000000000000000, 0.000000000000000000 ) ) ;
#7679=DIRECTION ( 'NONE',  ( -1.000000000000000000, 0.000000000000000000, 0.000000000000000000 ) ) ;
#7683=CARTESIAN_POINT ( 'NONE',  ( -42.00000000000000000, 25.22443390181683043, -1.500000000000000000 ) ) ;
#7684=DIRECTION ( 'NONE',  ( -0.000000000000000000, -0.000000000000000000, 1.000000000000000000 ) ) ;
#7687=CARTESIAN_POINT ( 'NONE',  ( 44.99999999999998579, 50.99999999999992184, 12.50000000000000000 ) ) ;
#7692=CARTESIAN_POINT ( 'NONE',  ( -36.00000000000001421, 50.99999999999999289, 0.5000000000000000000 ) ) ;
#7701=DIRECTION ( 'NONE',  ( 0.000000000000000000, 0.000000000000000000, 1.000000000000000000 ) ) ;
#7704=CARTESIAN_POINT ( 'NONE',  ( 40.23082370883258818, -29.49999999999999645, -3.000000000000000000 ) ) ;
#7717=DIRECTION ( 'NONE',  ( 0.7052211081716905916, 0.7089874389501501506, -0.000000000000000000 ) ) ;
#7718=PLANE ( 'NONE',  #1305 ) ;
#7735=ORIENTED_EDGE ( 'NONE', *, *, #12229, .T. ) ;
#7741=EDGE_LOOP ( 'NONE', ( #7864, #4787 ) ) ;
#7744=ORIENTED_EDGE ( 'NONE', *, *, #12371, .F. ) ;
#7745=CARTESIAN_POINT ( 'NONE',  ( -24.75000000000000000, 29.50000000000000000, -2.224999999999995204 ) ) ;
#7747=DIRECTION ( 'NONE',  ( -0.000000000000000000, -0.000000000000000000, -1.000000000000000000 ) ) ;
#7748=DIRECTION ( 'NONE',  ( -0.000000000000000000, -0.000000000000000000, 1.000000000000000000 ) ) ;
#7750=CARTESIAN_POINT ( 'NONE',  ( -44.00000000000001421, 50.99999999999999289, 0.000000000000000000 ) ) ;
#7755=EDGE_CURVE ( 'NONE', #10996, #10096, #5962, .T. ) ;
#7759=CIRCLE ( 'NONE', #17120, 4.499999999999997335 ) ;
#7767=CARTESIAN_POINT ( 'NONE',  ( 0.000000000000000000, -45.00000000000000000, -8.673617379884035472E-16 ) ) ;
#7768=DIRECTION ( 'NONE',  ( -0.000000000000000000, -0.000000000000000000, -1.000000000000000000 ) ) ;
#7773=EDGE_LOOP ( 'NONE', ( #2399, #13908, #9360, #17725 ) ) ;
#7774=ORIENTED_EDGE ( 'NONE', *, *, #5985, .T. ) ;
#7785=CARTESIAN_POINT ( 'NONE',  ( 10.00000000000000888, 15.50000000000000000, -2.999999999999999112 ) ) ;
#7786=DIRECTION ( 'NONE',  ( 1.000000000000000000, 0.000000000000000000, -0.000000000000000000 ) ) ;
#7787=ORIENTED_EDGE ( 'NONE', *, *, #5918, .T. ) ;
#7796=FACE_OUTER_BOUND ( 'NONE', #8853, .T. ) ;
#7807=DIRECTION ( 'NONE',  ( -0.7052211081716904806, 0.7089874389501500396, 0.000000000000000000 ) ) ;
#7826=ORIENTED_EDGE ( 'NONE', *, *, #6276, .T. ) ;
#7827=CARTESIAN_POINT ( 'NONE',  ( 3.890962118697714531E-15, 15.50000000000000000, 7.700000000000001954 ) ) ;
#7828=DIRECTION ( 'NONE',  ( 0.000000000000000000, 0.000000000000000000, 1.000000000000000000 ) ) ;
#7833=EDGE_LOOP ( 'NONE', ( #15436, #11847, #22310, #23853 ) ) ;
#7838=AXIS2_PLACEMENT_3D ( 'NONE', #10342, #6206, #13767 ) ;
#7841=AXIS2_PLACEMENT_3D ( 'NONE', #22188, #7747, #5576 ) ;
#7842=DIRECTION ( 'NONE',  ( -0.000000000000000000, -0.000000000000000000, -1.000000000000000000 ) ) ;
#7854=DIRECTION ( 'NONE',  ( 1.000000000000000000, 0.000000000000000000, 0.000000000000000000 ) ) ;
#7855=DIRECTION ( 'NONE',  ( 0.000000000000000000, 0.000000000000000000, 1.000000000000000000 ) ) ;
#7858=CARTESIAN_POINT ( 'NONE',  ( -41.73082370883257397, -27.62204025492845361, 0.000000000000000000 ) ) ;
#7864=ORIENTED_EDGE ( 'NONE', *, *, #1211, .F. ) ;
#7866=AXIS2_PLACEMENT_3D ( 'NONE', #7107, #6990, #21654 ) ;
#7869=EDGE_LOOP ( 'NONE', ( #16866, #23521, #14037, #6581 ) ) ;
#7883=VECTOR ( 'NONE', #9380, 1000.000000000000000 ) ;
#7887=DIRECTION ( 'NONE',  ( 0.000000000000000000, 0.000000000000000000, -1.000000000000000000 ) ) ;
#7890=AXIS2_PLACEMENT_3D ( 'NONE', #2373, #9790, #17256 ) ;
#7896=ORIENTED_EDGE ( 'NONE', *, *, #13025, .F. ) ;
#7903=AXIS2_PLACEMENT_3D ( 'NONE', #16290, #5189, #1542 ) ;
#7906=AXIS2_PLACEMENT_3D ( 'NONE', #3456, #5159, #22010 ) ;
#7910=CIRCLE ( 'NONE', #23517, 8.000000000000000000 ) ;
#7914=FACE_BOUND ( 'NONE', #22660, .T. ) ;
#7919=DIRECTION ( 'NONE',  ( 0.000000000000000000, 0.000000000000000000, 1.000000000000000000 ) ) ;
#7930=VECTOR ( 'NONE', #21820, 1000.000000000000000 ) ;
#7936=VECTOR ( 'NONE', #4662, 1000.000000000000000 ) ;
#7938=CIRCLE ( 'NONE', #11435, 1.500000000000000000 ) ;
#7941=DIRECTION ( 'NONE',  ( -0.000000000000000000, -0.000000000000000000, -1.000000000000000000 ) ) ;
#7960=VECTOR ( 'NONE', #13701, 1000.000000000000000 ) ;
#7961=DIRECTION ( 'NONE',  ( -0.000000000000000000, -0.000000000000000000, -1.000000000000000000 ) ) ;
#7967=ORIENTED_EDGE ( 'NONE', *, *, #12904, .F. ) ;
#7974=CIRCLE ( 'NONE', #21643, 1.500000000000001998 ) ;
#7980=FACE_BOUND ( 'NONE', #13855, .T. ) ;
#7982=DIRECTION ( 'NONE',  ( -0.000000000000000000, -0.000000000000000000, -1.000000000000000000 ) ) ;
#7985=ADVANCED_FACE ( 'NONE', ( #9741 ), #20889, .F. ) ;
#7986=CARTESIAN_POINT ( 'NONE',  ( -33.24999999999999289, -29.50000000000000000, 12.50000000000000000 ) ) ;
#7990=DIRECTION ( 'NONE',  ( 0.000000000000000000, 0.000000000000000000, 1.000000000000000000 ) ) ;
#7991=AXIS2_PLACEMENT_3D ( 'NONE', #6219, #621, #23193 ) ;
#7994=DIRECTION ( 'NONE',  ( -0.000000000000000000, -0.000000000000000000, -1.000000000000000000 ) ) ;
#8005=AXIS2_PLACEMENT_3D ( 'NONE', #5978, #22344, #13412 ) ;
#8011=PLANE ( 'NONE',  #8710 ) ;
#8018=DIRECTION ( 'NONE',  ( -1.000000000000000000, 0.000000000000000000, 0.000000000000000000 ) ) ;
#8021=CARTESIAN_POINT ( 'NONE',  ( -28.99999999999999645, 29.50000000000000000, -3.000000000000000000 ) ) ;
#8022=DIRECTION ( 'NONE',  ( -0.7052211081716905916, -0.7089874389501501506, -0.000000000000000000 ) ) ;
#8026=AXIS2_PLACEMENT_3D ( 'NONE', #22223, #23583, #5492 ) ;
#8027=AXIS2_PLACEMENT_3D ( 'NONE', #10363, #20012, #3293 ) ;
#8028=ORIENTED_EDGE ( 'NONE', *, *, #268, .T. ) ;
#8031=EDGE_CURVE ( 'NONE', #11436, #16760, #7127, .T. ) ;
#8034=DIRECTION ( 'NONE',  ( 1.000000000000000000, 0.000000000000000000, 0.000000000000000000 ) ) ;
#8035=EDGE_CURVE ( 'NONE', #5111, #10256, #10231, .T. ) ;
#8037=AXIS2_PLACEMENT_3D ( 'NONE', #21012, #4304, #6505 ) ;
#8043=ORIENTED_EDGE ( 'NONE', *, *, #6106, .T. ) ;
#8047=CARTESIAN_POINT ( 'NONE',  ( -40.23082370883258108, -27.62204025492846071, -3.000000000000000000 ) ) ;
#8051=LINE ( 'NONE', #17338, #17356 ) ;
#8057=CARTESIAN_POINT ( 'NONE',  ( 0.000000000000000000, 45.00000000000000000, -8.673617379884035472E-16 ) ) ;
#8070=DIRECTION ( 'NONE',  ( -1.000000000000000000, 0.000000000000000000, 0.000000000000000000 ) ) ;
#8071=DIRECTION ( 'NONE',  ( -0.7052211081716905916, 0.7089874389501501506, 0.000000000000000000 ) ) ;
#8072=ORIENTED_EDGE ( 'NONE', *, *, #15623, .T. ) ;
#8074=CARTESIAN_POINT ( 'NONE',  ( -40.23082370883260239, 29.50000000000000711, -1.500000000000000000 ) ) ;
#8101=VECTOR ( 'NONE', #18601, 1000.000000000000000 ) ;
#8108=EDGE_CURVE ( 'NONE', #1766, #3022, #8538, .T. ) ;
#8112=ORIENTED_EDGE ( 'NONE', *, *, #17664, .F. ) ;
#8113=EDGE_CURVE ( 'NONE', #1818, #23864, #14140, .T. ) ;
#8123=FACE_OUTER_BOUND ( 'NONE', #3167, .T. ) ;
#8129=CYLINDRICAL_SURFACE ( 'NONE', #11082, 1.500000000000001332 ) ;
#8147=CARTESIAN_POINT ( 'NONE',  ( 30.16774287754691386, -40.66994976491903913, -3.000000000000000000 ) ) ;
#8151=CARTESIAN_POINT ( 'NONE',  ( -40.23082370883260239, 29.50000000000000711, -3.000000000000000000 ) ) ;
#8155=ORIENTED_EDGE ( 'NONE', *, *, #2601, .T. ) ;
#8159=CYLINDRICAL_SURFACE ( 'NONE', #148, 1.500000000000000000 ) ;
#8161=AXIS2_PLACEMENT_3D ( 'NONE', #14045, #5029, #23338 ) ;
#8179=EDGE_LOOP ( 'NONE', ( #1378, #10106 ) ) ;
#8180=CARTESIAN_POINT ( 'NONE',  ( 15.00000000000000355, 15.50000000000000000, 7.700000000000001954 ) ) ;
#8185=ORIENTED_EDGE ( 'NONE', *, *, #1, .F. ) ;
#8196=LINE ( 'NONE', #19453, #1721 ) ;
#8215=EDGE_CURVE ( 'NONE', #6174, #17524, #2047, .T. ) ;
#8222=ORIENTED_EDGE ( 'NONE', *, *, #23513, .T. ) ;
#8240=CYLINDRICAL_SURFACE ( 'NONE', #2598, 8.999999999999994671 ) ;
#8252=AXIS2_PLACEMENT_3D ( 'NONE', #3184, #16353, #20382 ) ;
#8254=AXIS2_PLACEMENT_3D ( 'NONE', #8021, #7768, #6207 ) ;
#8263=VERTEX_POINT ( 'NONE', #8651 ) ;
#8273=CIRCLE ( 'NONE', #13737, 8.000000000000000000 ) ;
#8274=CIRCLE ( 'NONE', #21929, 17.25000000000000000 ) ;
#8286=ADVANCED_FACE ( 'NONE', ( #14500 ), #16453, .F. ) ;
#8288=ORIENTED_EDGE ( 'NONE', *, *, #606, .F. ) ;
#8291=DIRECTION ( 'NONE',  ( -1.000000000000000000, 0.000000000000000000, 0.000000000000000000 ) ) ;
#8294=DIRECTION ( 'NONE',  ( 0.000000000000000000, 0.000000000000000000, 1.000000000000000000 ) ) ;
#8296=TOROIDAL_SURFACE ( 'NONE', #15303, 3.500000000000001776, 1.500000000000000000 ) ;
#8299=AXIS2_PLACEMENT_3D ( 'NONE', #23642, #21904, #16179 ) ;
#8306=VECTOR ( 'NONE', #3525, 1000.000000000000000 ) ;
#8324=VECTOR ( 'NONE', #18377, 1000.000000000000000 ) ;
#8327=ORIENTED_EDGE ( 'NONE', *, *, #12173, .F. ) ;
#8329=DIRECTION ( 'NONE',  ( -0.000000000000000000, -0.000000000000000000, -1.000000000000000000 ) ) ;
#8330=DIRECTION ( 'NONE',  ( 0.000000000000000000, 0.000000000000000000, 1.000000000000000000 ) ) ;
#8332=ORIENTED_EDGE ( 'NONE', *, *, #15527, .F. ) ;
#8335=CARTESIAN_POINT ( 'NONE',  ( -41.73082370883260950, 27.62204025492845716, 0.000000000000000000 ) ) ;
#8345=VECTOR ( 'NONE', #23886, 1000.000000000000000 ) ;
#8355=DIRECTION ( 'NONE',  ( -1.000000000000000000, 0.000000000000000000, 0.000000000000000000 ) ) ;
#8358=CARTESIAN_POINT ( 'NONE',  ( 29.00000000000000355, -29.50000000000000000, -3.000000000000000000 ) ) ;
#8360=CIRCLE ( 'NONE', #13426, 1.499999999999999778 ) ;
#8369=FACE_OUTER_BOUND ( 'NONE', #12248, .T. ) ;
#8394=DIRECTION ( 'NONE',  ( -0.000000000000000000, -0.000000000000000000, 1.000000000000000000 ) ) ;
#8397=ORIENTED_EDGE ( 'NONE', *, *, #22614, .F. ) ;
#8403=AXIS2_PLACEMENT_3D ( 'NONE', #14766, #5270, #1501 ) ;
#8413=ADVANCED_FACE ( 'NONE', ( #9719 ), #4148, .F. ) ;
#8418=ORIENTED_EDGE ( 'NONE', *, *, #14880, .T. ) ;
#8420=DIRECTION ( 'NONE',  ( 0.000000000000000000, 0.000000000000000000, 1.000000000000000000 ) ) ;
#8425=CARTESIAN_POINT ( 'NONE',  ( 41.73082370883260239, 27.62204025492843940, -1.500000000000000000 ) ) ;
#8429=ORIENTED_EDGE ( 'NONE', *, *, #13213, .F. ) ;
#8442=ADVANCED_FACE ( 'NONE', ( #17540 ), #838, .T. ) ;
#8447=DIRECTION ( 'NONE',  ( 0.8571673007021120005, 1.049727191138618326E-16, -0.5150380749100547106 ) ) ;
#8450=VERTEX_POINT ( 'NONE', #10207 ) ;
#8451=CARTESIAN_POINT ( 'NONE',  ( 31.49999999999999289, 50.99999999999999289, 12.50000000000000000 ) ) ;
#8452=AXIS2_PLACEMENT_3D ( 'NONE', #9151, #3182, #10612 ) ;
#8461=FACE_OUTER_BOUND ( 'NONE', #3312, .T. ) ;
#8478=ORIENTED_EDGE ( 'NONE', *, *, #11142, .F. ) ;
#8487=DIRECTION ( 'NONE',  ( -1.000000000000000000, 0.000000000000000000, 0.000000000000000000 ) ) ;
#8497=EDGE_CURVE ( 'NONE', #13580, #1785, #21462, .T. ) ;
#8511=ORIENTED_EDGE ( 'NONE', *, *, #5103, .F. ) ;
#8512=CARTESIAN_POINT ( 'NONE',  ( -31.50000000000001421, 50.99999999999999289, 12.50000000000000000 ) ) ;
#8519=CARTESIAN_POINT ( 'NONE',  ( 24.75000000000000711, -29.50000000000000000, 12.50000000000000000 ) ) ;
#8520=EDGE_CURVE ( 'NONE', #1759, #13616, #10248, .T. ) ;
#8533=CARTESIAN_POINT ( 'NONE',  ( 35.99999999999999289, 50.99999999999999289, 0.5000000000000000000 ) ) ;
#8538=LINE ( 'NONE', #8047, #10225 ) ;
#8552=LINE ( 'NONE', #15997, #19347 ) ;
#8558=EDGE_LOOP ( 'NONE', ( #13973, #20598, #10622, #21811 ) ) ;
#8587=EDGE_LOOP ( 'NONE', ( #21671, #23043, #23181, #24067 ) ) ;
#8591=TOROIDAL_SURFACE ( 'NONE', #8985, 3.500000000000001776, 1.500000000000000000 ) ;
#8607=VECTOR ( 'NONE', #19294, 1000.000000000000000 ) ;
#8617=DIRECTION ( 'NONE',  ( 0.000000000000000000, 0.000000000000000000, -1.000000000000000000 ) ) ;
#8627=AXIS2_PLACEMENT_3D ( 'NONE', #7012, #11241, #1430 ) ;
#8633=CARTESIAN_POINT ( 'NONE',  ( -43.50000000000001421, 50.99999999999995026, 0.000000000000000000 ) ) ;
#8634=DIRECTION ( 'NONE',  ( 0.000000000000000000, 0.000000000000000000, -1.000000000000000000 ) ) ;
#8646=ADVANCED_FACE ( 'NONE', ( #19987 ), #8296, .F. ) ;
#8648=ADVANCED_FACE ( 'NONE', ( #10695 ), #1462, .F. ) ;
#8651=CARTESIAN_POINT ( 'NONE',  ( -40.23082370883257397, -29.50000000000000711, -1.500000000000000000 ) ) ;
#8671=EDGE_CURVE ( 'NONE', #1091, #6942, #23770, .T. ) ;
#8691=DIRECTION ( 'NONE',  ( -0.000000000000000000, -0.000000000000000000, 1.000000000000000000 ) ) ;
#8701=AXIS2_PLACEMENT_3D ( 'NONE', #6529, #7828, #4209 ) ;
#8710=AXIS2_PLACEMENT_3D ( 'NONE', #15460, #13389, #20854 ) ;
#8718=CARTESIAN_POINT ( 'NONE',  ( 29.00000000000000000, 29.50000000000000000, -3.000000000000000000 ) ) ;
#8722=AXIS2_PLACEMENT_3D ( 'NONE', #18583, #11465, #9381 ) ;
#8729=VERTEX_POINT ( 'NONE', #15071 ) ;
#8736=EDGE_CURVE ( 'NONE', #18312, #23135, #18390, .T. ) ;
#8739=EDGE_CURVE ( 'NONE', #13946, #1091, #20834, .T. ) ;
#8743=ADVANCED_FACE ( 'NONE', ( #11532 ), #22295, .F. ) ;
#8745=VECTOR ( 'NONE', #20669, 999.9999999999998863 ) ;
#8749=VECTOR ( 'NONE', #9834, 1000.000000000000114 ) ;
#8750=DIRECTION ( 'NONE',  ( 1.000000000000000000, 0.000000000000000000, 0.000000000000000000 ) ) ;
#8751=ORIENTED_EDGE ( 'NONE', *, *, #4125, .T. ) ;
#8756=DIRECTION ( 'NONE',  ( -0.000000000000000000, -0.000000000000000000, -1.000000000000000000 ) ) ;
#8766=VECTOR ( 'NONE', #23110, 1000.000000000000000 ) ;
#8803=AXIS2_PLACEMENT_3D ( 'NONE', #10361, #14740, #10933 ) ;
#8821=CARTESIAN_POINT ( 'NONE',  ( -40.66734255040738333, 26.56420859267091927, -3.000000000000000000 ) ) ;
#8823=DIRECTION ( 'NONE',  ( 0.000000000000000000, 0.000000000000000000, -1.000000000000000000 ) ) ;
#8831=DIRECTION ( 'NONE',  ( -1.000000000000000000, 0.000000000000000000, 0.000000000000000000 ) ) ;
#8835=DIRECTION ( 'NONE',  ( -0.000000000000000000, -0.000000000000000000, 1.000000000000000000 ) ) ;
#8840=DIRECTION ( 'NONE',  ( 0.7052211081716915908, -0.7089874389501490404, 0.000000000000000000 ) ) ;
#8853=EDGE_LOOP ( 'NONE', ( #14283, #9883, #17843, #14807 ) ) ;
#8854=PRODUCT_DEFINITION_SHAPE ( 'NONE', 'NONE',  #10008 ) ;
#8859=CARTESIAN_POINT ( 'NONE',  ( 35.99999999999999289, 50.99999999999999289, 0.000000000000000000 ) ) ;
#8868=CARTESIAN_POINT ( 'NONE',  ( 29.00000000000000000, 29.50000000000000000, -3.000000000000000000 ) ) ;
#8871=CARTESIAN_POINT ( 'NONE',  ( 41.73082370883257397, -27.62204025492843940, -3.000000000000000000 ) ) ;
#8887=AXIS2_PLACEMENT_3D ( 'NONE', #15063, #16769, #14820 ) ;
#8890=DIRECTION ( 'NONE',  ( 0.000000000000000000, 0.000000000000000000, -1.000000000000000000 ) ) ;
#8892=DIRECTION ( 'NONE',  ( -0.000000000000000000, -0.000000000000000000, -1.000000000000000000 ) ) ;
#8895=CYLINDRICAL_SURFACE ( 'NONE', #2395, 1.499999999999994449 ) ;
#8902=DIRECTION ( 'NONE',  ( -1.000000000000000000, 0.000000000000000000, 0.000000000000000000 ) ) ;
#8903=EDGE_LOOP ( 'NONE', ( #4996, #11895, #15586, #8984 ) ) ;
#8907=FACE_OUTER_BOUND ( 'NONE', #15635, .T. ) ;
#8914=LINE ( 'NONE', #7087, #13355 ) ;
#8917=ORIENTED_EDGE ( 'NONE', *, *, #21348, .T. ) ;
#8919=EDGE_CURVE ( 'NONE', #8263, #4207, #12537, .T. ) ;
#8920=TOROIDAL_SURFACE ( 'NONE', #12028, 3.500000000000001776, 1.500000000000000000 ) ;
#8921=CARTESIAN_POINT ( 'NONE',  ( -36.00000000000001421, 50.99999999999999289, 0.5000000000000000000 ) ) ;
#8923=ORIENTED_EDGE ( 'NONE', *, *, #18999, .F. ) ;
#8943=ADVANCED_FACE ( 'NONE', ( #7914, #19414, #22836, #2207, #2691, #10105, #17078, #378 ), #6223, .F. ) ;
#8960=ORIENTED_EDGE ( 'NONE', *, *, #17629, .T. ) ;
#8962=DIRECTION ( 'NONE',  ( -0.7071067811865474617, 0.000000000000000000, -0.7071067811865474617 ) ) ;
#8974=CARTESIAN_POINT ( 'NONE',  ( 15.00000000000000355, 15.50000000000000000, 7.700000000000001954 ) ) ;
#8983=ORIENTED_EDGE ( 'NONE', *, *, #4062, .T. ) ;
#8984=ORIENTED_EDGE ( 'NONE', *, *, #7438, .T. ) ;
#8985=AXIS2_PLACEMENT_3D ( 'NONE', #703, #15820, #19616 ) ;
#8988=EDGE_LOOP ( 'NONE', ( #22751, #18238, #2894 ) ) ;
#9010=CARTESIAN_POINT ( 'NONE',  ( 0.000000000000000000, -45.00000000000000000, -3.000000000000000000 ) ) ;
#9014=EDGE_LOOP ( 'NONE', ( #22353, #20462, #14598, #12246 ) ) ;
#9016=EDGE_LOOP ( 'NONE', ( #3041, #2493 ) ) ;
#9021=EDGE_CURVE ( 'NONE', #6097, #18287, #6716, .T. ) ;
#9027=AXIS2_PLACEMENT_3D ( 'NONE', #5858, #18926, #13422 ) ;
#9031=CARTESIAN_POINT ( 'NONE',  ( -28.99999999999998579, -29.50000000000000711, -3.000000000000000000 ) ) ;
#9046=AXIS2_PLACEMENT_3D ( 'NONE', #9550, #3587, #24086 ) ;
#9051=CARTESIAN_POINT ( 'NONE',  ( 40.49999999999998579, -51.00000000000000711, 0.5000000000000004441 ) ) ;
#9075=FACE_OUTER_BOUND ( 'NONE', #17065, .T. ) ;
#9084=AXIS2_PLACEMENT_3D ( 'NONE', #1620, #23952, #4823 ) ;
#9086=CIRCLE ( 'NONE', #23913, 12.73082370883259884 ) ;
#9096=AXIS2_PLACEMENT_3D ( 'NONE', #9995, #17451, #17562 ) ;
#9101=VECTOR ( 'NONE', #9567, 1000.000000000000000 ) ;
#9108=CARTESIAN_POINT ( 'NONE',  ( -24.75000000000000000, 29.50000000000000000, 14.00000000000000178 ) ) ;
#9123=DIRECTION ( 'NONE',  ( 1.000000000000000000, 0.000000000000000000, 0.000000000000000000 ) ) ;
#9133=DIRECTION ( 'NONE',  ( 1.000000000000000000, 0.000000000000000000, 0.000000000000000000 ) ) ;
#9141=DIRECTION ( 'NONE',  ( -0.000000000000000000, -0.000000000000000000, -1.000000000000000000 ) ) ;
#9151=CARTESIAN_POINT ( 'NONE',  ( 29.00000000000000355, -29.50000000000000000, -2.224999999999995204 ) ) ;
#9168=PLANE ( 'NONE',  #19196 ) ;
#9172=LINE ( 'NONE', #3561, #11439 ) ;
#9173=DIRECTION ( 'NONE',  ( 0.000000000000000000, 0.000000000000000000, 1.000000000000000000 ) ) ;
#9176=ADVANCED_FACE ( 'NONE', ( #6202 ), #9836, .F. ) ;
#9188=ORIENTED_EDGE ( 'NONE', *, *, #15903, .T. ) ;
#9198=CARTESIAN_POINT ( 'NONE',  ( -40.50000000000000000, -51.00000000000000711, 12.50000000000000000 ) ) ;
#9199=DIRECTION ( 'NONE',  ( -1.000000000000000000, 0.000000000000000000, 0.000000000000000000 ) ) ;
#9203=FACE_BOUND ( 'NONE', #21275, .T. ) ;
#9211=AXIS2_PLACEMENT_3D ( 'NONE', #3694, #2099, #519 ) ;
#9213=DIRECTION ( 'NONE',  ( 0.000000000000000000, -1.000000000000000000, 0.000000000000000000 ) ) ;
#9215=EDGE_LOOP ( 'NONE', ( #17313, #16994, #5425, #12479 ) ) ;
#9218=ORIENTED_EDGE ( 'NONE', *, *, #20515, .T. ) ;
#9234=LINE ( 'NONE', #20955, #5578 ) ;
#9235=ADVANCED_FACE ( 'NONE', ( #18899 ), #9605, .F. ) ;
#9240=ORIENTED_EDGE ( 'NONE', *, *, #20385, .F. ) ;
#9247=DIRECTION ( 'NONE',  ( -1.000000000000000000, 0.000000000000000000, 0.000000000000000000 ) ) ;
#9248=ADVANCED_FACE ( 'NONE', ( #2412 ), #21458, .F. ) ;
#9256=CARTESIAN_POINT ( 'NONE',  ( -36.00000000000001421, 50.99999999999999289, 12.50000000000000000 ) ) ;
#9258=CONICAL_SURFACE ( 'NONE', #10839, 4.249999999999993783, 1.029744258676653645 ) ;
#9262=DIRECTION ( 'NONE',  ( 0.000000000000000000, 0.000000000000000000, 1.000000000000000000 ) ) ;
#9268=CIRCLE ( 'NONE', #13573, 40.00000000000000000 ) ;
#9286=CARTESIAN_POINT ( 'NONE',  ( -24.75000000000000000, -29.50000000000000000, -2.224999999999995204 ) ) ;
#9294=EDGE_CURVE ( 'NONE', #6856, #4207, #23302, .T. ) ;
#9299=EDGE_CURVE ( 'NONE', #15211, #17944, #12291, .T. ) ;
#9307=CARTESIAN_POINT ( 'NONE',  ( 24.75000000000000355, 29.50000000000000000, -3.000000000000000000 ) ) ;
#9321=VERTEX_POINT ( 'NONE', #19761 ) ;
#9322=DIRECTION ( 'NONE',  ( 1.000000000000000000, 0.000000000000000000, 0.000000000000000000 ) ) ;
#9327=ADVANCED_FACE ( 'NONE', ( #10457 ), #17916, .F. ) ;
#9330=LINE ( 'NONE', #7493, #504 ) ;
#9336=CARTESIAN_POINT ( 'NONE',  ( 35.99999999999999289, -51.00000000000000711, 12.50000000000000000 ) ) ;
#9345=DIRECTION ( 'NONE',  ( 0.000000000000000000, 0.000000000000000000, -1.000000000000000000 ) ) ;
#9347=DIRECTION ( 'NONE',  ( -1.000000000000000000, 0.000000000000000000, 0.000000000000000000 ) ) ;
#9348=EDGE_CURVE ( 'NONE', #12511, #6174, #12407, .T. ) ;
#9357=CARTESIAN_POINT ( 'NONE',  ( -2.024999999999999911, 45.00000000000000000, -3.000000000000000000 ) ) ;
#9360=ORIENTED_EDGE ( 'NONE', *, *, #21450, .F. ) ;
#9372=AXIS2_PLACEMENT_3D ( 'NONE', #4354, #7854, #22905 ) ;
#9380=DIRECTION ( 'NONE',  ( -0.000000000000000000, -0.000000000000000000, -1.000000000000000000 ) ) ;
#9381=DIRECTION ( 'NONE',  ( -1.000000000000000000, 0.000000000000000000, 0.000000000000000000 ) ) ;
#9390=CARTESIAN_POINT ( 'NONE',  ( 0.000000000000000000, 45.00000000000000000, -2.974999999999996092 ) ) ;
#9391=EDGE_LOOP ( 'NONE', ( #15078, #19364, #5347, #23669 ) ) ;
#9392=EDGE_CURVE ( 'NONE', #22141, #13616, #16305, .T. ) ;
#9395=ORIENTED_EDGE ( 'NONE', *, *, #5638, .T. ) ;
#9397=CARTESIAN_POINT ( 'NONE',  ( -36.00000000000000711, -51.00000000000000711, 12.50000000000000000 ) ) ;
#9400=ORIENTED_EDGE ( 'NONE', *, *, #14454, .T. ) ;
#9412=EDGE_CURVE ( 'NONE', #22424, #14048, #8273, .T. ) ;
#9413=FACE_BOUND ( 'NONE', #23542, .T. ) ;
#9418=EDGE_LOOP ( 'NONE', ( #7146, #5417, #14273, #8429 ) ) ;
#9421=ORIENTED_EDGE ( 'NONE', *, *, #6689, .T. ) ;
#9428=AXIS2_PLACEMENT_3D ( 'NONE', #7289, #3398, #1686 ) ;
#9453=DIRECTION ( 'NONE',  ( -0.000000000000000000, -0.000000000000000000, -1.000000000000000000 ) ) ;
#9463=EDGE_LOOP ( 'NONE', ( #23242, #3793 ) ) ;
#9467=CIRCLE ( 'NONE', #8701, 12.73082370883260594 ) ;
#9468=AXIS2_PLACEMENT_3D ( 'NONE', #207, #3739, #2376 ) ;
#9469=VECTOR ( 'NONE', #19926, 1000.000000000000000 ) ;
#9489=VECTOR ( 'NONE', #12469, 1000.000000000000000 ) ;
#9493=ORIENTED_EDGE ( 'NONE', *, *, #22417, .F. ) ;
#9507=EDGE_CURVE ( 'NONE', #4705, #7322, #9330, .T. ) ;
#9511=DIRECTION ( 'NONE',  ( 0.000000000000000000, 0.000000000000000000, 1.000000000000000000 ) ) ;
#9513=CIRCLE ( 'NONE', #20438, 4.499999999999997335 ) ;
#9524=CARTESIAN_POINT ( 'NONE',  ( 30.68762588338046982, -45.64284848299539732, -1.500000000000000000 ) ) ;
#9531=VECTOR ( 'NONE', #8447, 1000.000000000000000 ) ;
#9540=ORIENTED_EDGE ( 'NONE', *, *, #5431, .F. ) ;
#9543=DIRECTION ( 'NONE',  ( -0.000000000000000000, -0.000000000000000000, -1.000000000000000000 ) ) ;
#9549=CARTESIAN_POINT ( 'NONE',  ( -40.23082370883260239, 29.50000000000000711, -3.000000000000000000 ) ) ;
#9550=CARTESIAN_POINT ( 'NONE',  ( 41.73082370883260239, 27.62204025492843940, -3.000000000000000000 ) ) ;
#9556=FACE_OUTER_BOUND ( 'NONE', #5473, .T. ) ;
#9566=CIRCLE ( 'NONE', #649, 4.249999999999996447 ) ;
#9567=DIRECTION ( 'NONE',  ( -0.000000000000000000, -0.000000000000000000, -1.000000000000000000 ) ) ;
#9570=DIRECTION ( 'NONE',  ( -1.000000000000000000, 0.000000000000000000, 0.000000000000000000 ) ) ;
#9580=EDGE_CURVE ( 'NONE', #12142, #8729, #15676, .T. ) ;
#9586=PLANE ( 'NONE',  #14192 ) ;
#9591=DIRECTION ( 'NONE',  ( 0.000000000000000000, 0.000000000000000000, 1.000000000000000000 ) ) ;
#9596=AXIS2_PLACEMENT_3D ( 'NONE', #18924, #11682, #8034 ) ;
#9601=CARTESIAN_POINT ( 'NONE',  ( -31.50000000000000711, -51.00000000000000711, 12.50000000000000000 ) ) ;
#9605=CYLINDRICAL_SURFACE ( 'NONE', #20356, 4.499999999999997335 ) ;
#9607=CARTESIAN_POINT ( 'NONE',  ( 40.23082370883260239, 27.62204025492844650, -3.000000000000000000 ) ) ;
#9609=CARTESIAN_POINT ( 'NONE',  ( -23.97499999999999787, -29.50000000000000000, -3.000000000000000000 ) ) ;
#9612=DIRECTION ( 'NONE',  ( -1.000000000000000000, 0.000000000000000000, 0.000000000000000000 ) ) ;
#9624=EDGE_CURVE ( 'NONE', #22141, #15940, #11392, .T. ) ;
#9627=AXIS2_PLACEMENT_3D ( 'NONE', #10274, #15400, #14065 ) ;
#9654=CARTESIAN_POINT ( 'NONE',  ( 15.00000000000000355, 15.50000000000000000, 7.700000000000001954 ) ) ;
#9655=ORIENTED_EDGE ( 'NONE', *, *, #20803, .T. ) ;
#9667=DIRECTION ( 'NONE',  ( -0.000000000000000000, -0.000000000000000000, -1.000000000000000000 ) ) ;
#9690=ORIENTED_EDGE ( 'NONE', *, *, #6233, .F. ) ;
#9700=ORIENTED_EDGE ( 'NONE', *, *, #19184, .F. ) ;
#9705=EDGE_CURVE ( 'NONE', #1921, #17955, #16487, .T. ) ;
#9711=LINE ( 'NONE', #13142, #16636 ) ;
#9712=CARTESIAN_POINT ( 'NONE',  ( -33.24999999999999289, -29.50000000000000000, -2.224999999999995204 ) ) ;
#9719=FACE_OUTER_BOUND ( 'NONE', #12894, .T. ) ;
#9724=CIRCLE ( 'NONE', #8161, 4.499999999999997335 ) ;
#9728=DIRECTION ( 'NONE',  ( 0.000000000000000000, -1.000000000000000000, 4.625929269271485322E-15 ) ) ;
#9729=CARTESIAN_POINT ( 'NONE',  ( -36.00000000000001421, 50.99999999999999289, 0.000000000000000000 ) ) ;
#9732=EDGE_CURVE ( 'NONE', #16017, #21225, #11893, .T. ) ;
#9736=ORIENTED_EDGE ( 'NONE', *, *, #4161, .T. ) ;
#9737=CIRCLE ( 'NONE', #11283, 11.23082370883259706 ) ;
#9741=FACE_OUTER_BOUND ( 'NONE', #12390, .T. ) ;
#9743=DIRECTION ( 'NONE',  ( 0.000000000000000000, 0.000000000000000000, -1.000000000000000000 ) ) ;
#9753=DIRECTION ( 'NONE',  ( -1.000000000000000000, 0.000000000000000000, 0.000000000000000000 ) ) ;
#9757=EDGE_CURVE ( 'NONE', #15653, #16665, #4416, .T. ) ;
#9766=CYLINDRICAL_SURFACE ( 'NONE', #2658, 8.000000000000000000 ) ;
#9767=VECTOR ( 'NONE', #3408, 1000.000000000000000 ) ;
#9775=FACE_OUTER_BOUND ( 'NONE', #19055, .T. ) ;
#9776=DIRECTION ( 'NONE',  ( -1.000000000000000000, 0.000000000000000000, 0.000000000000000000 ) ) ;
#9778=ORIENTED_EDGE ( 'NONE', *, *, #3577, .T. ) ;
#9782=ADVANCED_FACE ( 'NONE', ( #19729 ), #2859, .F. ) ;
#9790=DIRECTION ( 'NONE',  ( -0.000000000000000000, -0.000000000000000000, -1.000000000000000000 ) ) ;
#9794=EDGE_LOOP ( 'NONE', ( #21601, #18384, #19274, #4128 ) ) ;
#9797=DIRECTION ( 'NONE',  ( -1.000000000000000000, 0.000000000000000000, 0.000000000000000000 ) ) ;
#9804=FACE_OUTER_BOUND ( 'NONE', #3441, .T. ) ;
#9810=CIRCLE ( 'NONE', #19964, 51.49999999999999289 ) ;
#9818=ADVANCED_FACE ( 'NONE', ( #4482 ), #20080, .F. ) ;
#9820=VECTOR ( 'NONE', #3796, 1000.000000000000000 ) ;
#9821=EDGE_LOOP ( 'NONE', ( #23874, #11508, #21753, #11938 ) ) ;
#9826=PRODUCT_DEFINITION_CONTEXT ( 'detailed design', #4014, 'design' ) ;
#9827=CARTESIAN_POINT ( 'NONE',  ( 0.000000000000000000, 0.000000000000000000, -3.000000000000000000 ) ) ;
#9829=AXIS2_PLACEMENT_3D ( 'NONE', #8718, #807, #15671 ) ;
#9834=DIRECTION ( 'NONE',  ( 0.7052211081716895924, 0.7089874389501509278, -0.000000000000000000 ) ) ;
#9836=CYLINDRICAL_SURFACE ( 'NONE', #3576, 17.25000000000000000 ) ;
#9841=DIRECTION ( 'NONE',  ( -0.000000000000000000, -0.000000000000000000, -1.000000000000000000 ) ) ;
#9842=CARTESIAN_POINT ( 'NONE',  ( -41.73082370883260239, 27.62204025492845361, -3.000000000000000000 ) ) ;
#9843=CIRCLE ( 'NONE', #11404, 17.25000000000000000 ) ;
#9847=ORIENTED_EDGE ( 'NONE', *, *, #14057, .F. ) ;
#9854=CIRCLE ( 'NONE', #938, 4.249999999999996447 ) ;
#9859=AXIS2_PLACEMENT_3D ( 'NONE', #5064, #18127, #3908 ) ;
#9862=VECTOR ( 'NONE', #7717, 999.9999999999998863 ) ;
#9883=ORIENTED_EDGE ( 'NONE', *, *, #23015, .T. ) ;
#9890=CARTESIAN_POINT ( 'NONE',  ( -41.73082370883258108, -27.62204025492845716, -1.500000000000000000 ) ) ;
#9891=AXIS2_PLACEMENT_3D ( 'NONE', #12910, #20371, #16454 ) ;
#9895=DIRECTION ( 'NONE',  ( -0.000000000000000000, -0.000000000000000000, -1.000000000000000000 ) ) ;
#9899=ORIENTED_EDGE ( 'NONE', *, *, #9507, .T. ) ;
#9901=SPHERICAL_SURFACE ( 'NONE', #12759, 1.500000000000000000 ) ;
#9947=ORIENTED_EDGE ( 'NONE', *, *, #4288, .F. ) ;
#9960=CARTESIAN_POINT ( 'NONE',  ( 40.66734255040738333, 26.56420859267091217, -3.000000000000000000 ) ) ;
#9963=CARTESIAN_POINT ( 'NONE',  ( 78.19113660963670043, 9.032993985154128325, 0.000000000000000000 ) ) ;
#9987=EDGE_CURVE ( 'NONE', #22195, #1759, #3357, .T. ) ;
#9992=ADVANCED_FACE ( 'NONE', ( #864 ), #8159, .F. ) ;
#9995=CARTESIAN_POINT ( 'NONE',  ( 41.73082370883258818, -27.62204025492844650, -1.500000000000000000 ) ) ;
#10008=PRODUCT_DEFINITION ( 'UNKNOWN', '', #3373, #9826 ) ;
#10009=CARTESIAN_POINT ( 'NONE',  ( -33.24999999999999289, 29.50000000000000000, -2.224999999999995204 ) ) ;
#10010=ADVANCED_FACE ( 'NONE', ( #17331 ), #13928, .F. ) ;
#10014=LINE ( 'NONE', #8180, #16621 ) ;
#10015=EDGE_CURVE ( 'NONE', #19090, #12662, #10262, .T. ) ;
#10025=CARTESIAN_POINT ( 'NONE',  ( -28.00000000000001066, 50.99999999999999289, 0.5000000000000000000 ) ) ;
#10033=ORIENTED_EDGE ( 'NONE', *, *, #4941, .F. ) ;
#10036=ORIENTED_EDGE ( 'NONE', *, *, #19546, .T. ) ;
#10040=ORIENTED_EDGE ( 'NONE', *, *, #14351, .T. ) ;
#10056=DIRECTION ( 'NONE',  ( -1.000000000000000000, 0.000000000000000000, 0.000000000000000000 ) ) ;
#10057=CARTESIAN_POINT ( 'NONE',  ( 40.23082370883260239, 27.62204025492844650, -1.500000000000000000 ) ) ;
#10058=DIRECTION ( 'NONE',  ( 0.000000000000000000, 0.000000000000000000, -1.000000000000000000 ) ) ;
#10059=CARTESIAN_POINT ( 'NONE',  ( 28.99999999999999645, 29.49999999999999645, -3.000000000000000000 ) ) ;
#10064=ORIENTED_EDGE ( 'NONE', *, *, #10395, .F. ) ;
#10068=VERTEX_POINT ( 'NONE', #21965 ) ;
#10070=DIRECTION ( 'NONE',  ( -0.000000000000000000, -0.000000000000000000, -1.000000000000000000 ) ) ;
#10085=FACE_OUTER_BOUND ( 'NONE', #21775, .T. ) ;
#10096=VERTEX_POINT ( 'NONE', #21736 ) ;
#10102=CARTESIAN_POINT ( 'NONE',  ( 34.02500000000000568, -29.50000000000000000, -3.000000000000000000 ) ) ;
#10105=FACE_BOUND ( 'NONE', #23257, .T. ) ;
#10106=ORIENTED_EDGE ( 'NONE', *, *, #21028, .F. ) ;
#10109=CARTESIAN_POINT ( 'NONE',  ( -41.73082370883260239, 29.50000000000000711, -1.500000000000000000 ) ) ;
#10113=CARTESIAN_POINT ( 'NONE',  ( 35.99999999999999289, -51.00000000000000711, 12.50000000000000000 ) ) ;
#10116=CARTESIAN_POINT ( 'NONE',  ( 40.49999999999998579, 50.99999999999999289, 0.5000000000000004441 ) ) ;
#10121=DIRECTION ( 'NONE',  ( -1.000000000000000000, 0.000000000000000000, 0.000000000000000000 ) ) ;
#10131=CARTESIAN_POINT ( 'NONE',  ( 40.00000000000000711, 15.50000000000000533, 19.70000000000000284 ) ) ;
#10134=EDGE_LOOP ( 'NONE', ( #21887, #15593, #20262, #822 ) ) ;
#10136=LINE ( 'NONE', #2141, #9101 ) ;
#10138=FACE_OUTER_BOUND ( 'NONE', #14453, .T. ) ;
#10141=LINE ( 'NONE', #18970, #23861 ) ;
#10146=LINE ( 'NONE', #23112, #20413 ) ;
#10152=VERTEX_POINT ( 'NONE', #21487 ) ;
#10163=ORIENTED_EDGE ( 'NONE', *, *, #16375, .T. ) ;
#10167=DIRECTION ( 'NONE',  ( -0.000000000000000000, -0.000000000000000000, -1.000000000000000000 ) ) ;
#10171=DIRECTION ( 'NONE',  ( -1.000000000000000000, 0.000000000000000000, 0.000000000000000000 ) ) ;
#10182=ORIENTED_EDGE ( 'NONE', *, *, #5668, .F. ) ;
#10190=LINE ( 'NONE', #11654, #1133 ) ;
#10195=DIRECTION ( 'NONE',  ( 0.000000000000000000, 1.000000000000000000, 0.000000000000000000 ) ) ;
#10198=DIRECTION ( 'NONE',  ( -1.000000000000000000, 0.000000000000000000, 0.000000000000000000 ) ) ;
#10207=CARTESIAN_POINT ( 'NONE',  ( -27.89784171216405895, -41.49349862090491570, -1.500000000000000000 ) ) ;
#10225=VECTOR ( 'NONE', #15985, 1000.000000000000000 ) ;
#10231=CIRCLE ( 'NONE', #18039, 51.49999999999999289 ) ;
#10237=CARTESIAN_POINT ( 'NONE',  ( 41.73082370883257397, -29.49999999999999645, -1.500000000000000000 ) ) ;
#10238=APPLICATION_CONTEXT ( 'automotive_design' ) ;
#10239=EDGE_LOOP ( 'NONE', ( #20505, #8288, #17383, #4732 ) ) ;
#10246=DIRECTION ( 'NONE',  ( 0.000000000000000000, 0.000000000000000000, -1.000000000000000000 ) ) ;
#10248=CIRCLE ( 'NONE', #19631, 8.999999999999994671 ) ;
#10254=ORIENTED_EDGE ( 'NONE', *, *, #11767, .T. ) ;
#10256=VERTEX_POINT ( 'NONE', #14854 ) ;
#10262=CIRCLE ( 'NONE', #22748, 8.999999999999994671 ) ;
#10263=ORIENTED_EDGE ( 'NONE', *, *, #21348, .F. ) ;
#10269=ORIENTED_EDGE ( 'NONE', *, *, #12549, .F. ) ;
#10274=CARTESIAN_POINT ( 'NONE',  ( 0.000000000000000000, 0.000000000000000000, -3.000000000000000000 ) ) ;
#10281=ADVANCED_FACE ( 'NONE', ( #24034 ), #7459, .F. ) ;
#10288=DIRECTION ( 'NONE',  ( -1.000000000000000000, 0.000000000000000000, 0.000000000000000000 ) ) ;
#10294=AXIS2_PLACEMENT_3D ( 'NONE', #12611, #20302, #16387 ) ;
#10302=ORIENTED_EDGE ( 'NONE', *, *, #16676, .T. ) ;
#10305=DIRECTION ( 'NONE',  ( 0.000000000000000000, -1.000000000000000000, 0.000000000000000000 ) ) ;
#10306=EDGE_LOOP ( 'NONE', ( #18130, #7896, #231, #2860 ) ) ;
#10307=CARTESIAN_POINT ( 'NONE',  ( 41.73082370883260239, 27.62204025492844650, -1.500000000000000000 ) ) ;
#10312=CARTESIAN_POINT ( 'NONE',  ( 3.890962118697714531E-15, 15.50000000000000000, 19.70000000000000284 ) ) ;
#10317=DIRECTION ( 'NONE',  ( 1.000000000000000000, 0.000000000000000000, 0.000000000000000000 ) ) ;
#10329=EDGE_LOOP ( 'NONE', ( #21490, #8923, #21731, #16842 ) ) ;
#10333=CARTESIAN_POINT ( 'NONE',  ( 3.890962118697714531E-15, 15.50000000000000000, 16.70000000000000284 ) ) ;
#10334=CARTESIAN_POINT ( 'NONE',  ( 3.890962118697714531E-15, 15.50000000000000000, 19.70000000000000284 ) ) ;
#10336=ADVANCED_FACE ( 'NONE', ( #13532 ), #21345, .T. ) ;
#10342=CARTESIAN_POINT ( 'NONE',  ( 41.73082370883257397, -29.49999999999999645, -1.500000000000000000 ) ) ;
#10346=ORIENTED_EDGE ( 'NONE', *, *, #10714, .F. ) ;
#10349=ORIENTED_EDGE ( 'NONE', *, *, #4163, .T. ) ;
#10358=CARTESIAN_POINT ( 'NONE',  ( -2.024999999999999911, -45.00000000000000000, -3.000000000000000000 ) ) ;
#10359=ADVANCED_FACE ( 'NONE', ( #11926 ), #15469, .F. ) ;
#10360=CYLINDRICAL_SURFACE ( 'NONE', #2581, 4.499999999999997335 ) ;
#10361=CARTESIAN_POINT ( 'NONE',  ( -40.23082370883257397, -29.50000000000000711, -3.000000000000000000 ) ) ;
#10363=CARTESIAN_POINT ( 'NONE',  ( 29.00000000000000000, 29.50000000000000000, -2.224999999999995204 ) ) ;
#10373=DIRECTION ( 'NONE',  ( -0.000000000000000000, -0.000000000000000000, 1.000000000000000000 ) ) ;
#10381=FACE_OUTER_BOUND ( 'NONE', #12460, .T. ) ;
#10395=EDGE_CURVE ( 'NONE', #7322, #15518, #10590, .T. ) ;
#10408=ORIENTED_EDGE ( 'NONE', *, *, #8031, .T. ) ;
#10457=FACE_OUTER_BOUND ( 'NONE', #17381, .T. ) ;
#10464=CARTESIAN_POINT ( 'NONE',  ( -36.00000000000001421, 50.99999999999999289, 0.5000000000000000000 ) ) ;
#10471=ADVANCED_FACE ( 'NONE', ( #10085 ), #1333, .F. ) ;
#10475=DIRECTION ( 'NONE',  ( -0.7052211081716895924, -0.7089874389501509278, 0.000000000000000000 ) ) ;
#10480=ADVANCED_BREP_SHAPE_REPRESENTATION ( '', ( #18364, #8005 ), #15828 ) ;
#10490=ORIENTED_EDGE ( 'NONE', *, *, #13807, .F. ) ;
#10493=ORIENTED_EDGE ( 'NONE', *, *, #16476, .T. ) ;
#10511=CARTESIAN_POINT ( 'NONE',  ( 30.68762588338048403, 45.64284848299539732, -1.500000000000000000 ) ) ;
#10545=EDGE_CURVE ( 'NONE', #5796, #17727, #4754, .T. ) ;
#10549=ORIENTED_EDGE ( 'NONE', *, *, #3584, .T. ) ;
#10562=FACE_OUTER_BOUND ( 'NONE', #8587, .T. ) ;
#10563=ORIENTED_EDGE ( 'NONE', *, *, #12129, .T. ) ;
#10567=VERTEX_POINT ( 'NONE', #3145 ) ;
#10573=LINE ( 'NONE', #16423, #8345 ) ;
#10576=AXIS2_PLACEMENT_3D ( 'NONE', #5112, #20003, #9123 ) ;
#10580=ORIENTED_EDGE ( 'NONE', *, *, #21444, .T. ) ;
#10590=CIRCLE ( 'NONE', #8254, 5.025000000000002132 ) ;
#10597=ORIENTED_EDGE ( 'NONE', *, *, #20818, .F. ) ;
#10610=CIRCLE ( 'NONE', #12942, 4.249999999999996447 ) ;
#10612=DIRECTION ( 'NONE',  ( -1.000000000000000000, 0.000000000000000000, 0.000000000000000000 ) ) ;
#10622=ORIENTED_EDGE ( 'NONE', *, *, #12429, .T. ) ;
#10641=VECTOR ( 'NONE', #13587, 1000.000000000000000 ) ;
#10645=CIRCLE ( 'NONE', #153, 8.000000000000000000 ) ;
#10647=ORIENTED_EDGE ( 'NONE', *, *, #9624, .T. ) ;
#10649=VERTEX_POINT ( 'NONE', #5219 ) ;
#10654=ORIENTED_EDGE ( 'NONE', *, *, #6630, .F. ) ;
#10658=DIRECTION ( 'NONE',  ( 0.8571673007021118895, 1.049727191138618079E-16, -0.5150380749100549327 ) ) ;
#10664=DIRECTION ( 'NONE',  ( 1.000000000000000000, 0.000000000000000000, 0.000000000000000000 ) ) ;
#10668=DIRECTION ( 'NONE',  ( 0.9945797436152715720, 0.1039766011667100365, -0.000000000000000000 ) ) ;
#10675=PRODUCT_CONTEXT ( 'NONE', #10238, 'mechanical' ) ;
#10678=ORIENTED_EDGE ( 'NONE', *, *, #11142, .T. ) ;
#10685=CARTESIAN_POINT ( 'NONE',  ( 28.73477696352899358, -42.73830357953205095, -1.500000000000000000 ) ) ;
#10695=FACE_OUTER_BOUND ( 'NONE', #7869, .T. ) ;
#10701=CARTESIAN_POINT ( 'NONE',  ( 31.49999999999999289, -51.00000000000000711, 0.5000000000000004441 ) ) ;
#10703=ORIENTED_EDGE ( 'NONE', *, *, #6763, .T. ) ;
#10713=FACE_OUTER_BOUND ( 'NONE', #11618, .T. ) ;
#10714=EDGE_CURVE ( 'NONE', #1952, #1785, #1294, .T. ) ;
#10723=DIRECTION ( 'NONE',  ( 1.000000000000000000, 0.000000000000000000, 0.000000000000000000 ) ) ;
#10726=LINE ( 'NONE', #6965, #2517 ) ;
#10730=LINE ( 'NONE', #5259, #15395 ) ;
#10739=DIRECTION ( 'NONE',  ( 0.000000000000000000, 1.000000000000000000, 0.000000000000000000 ) ) ;
#10746=CIRCLE ( 'NONE', #14656, 1.999999999999997113 ) ;
#10751=FACE_OUTER_BOUND ( 'NONE', #9794, .T. ) ;
#10762=CARTESIAN_POINT ( 'NONE',  ( -40.66734255040739043, 26.56420859267092283, -3.000000000000000000 ) ) ;
#10767=VERTEX_POINT ( 'NONE', #10057 ) ;
#10775=DIRECTION ( 'NONE',  ( -0.000000000000000000, -0.000000000000000000, -1.000000000000000000 ) ) ;
#10777=CARTESIAN_POINT ( 'NONE',  ( 35.99999999999992184, -60.00000000000000000, 12.50000000000000000 ) ) ;
#10782=ADVANCED_FACE ( 'NONE', ( #18871 ), #17146, .F. ) ;
#10787=ORIENTED_EDGE ( 'NONE', *, *, #139, .F. ) ;
#10791=ADVANCED_FACE ( 'NONE', ( #9804 ), #15209, .F. ) ;
#10804=DIRECTION ( 'NONE',  ( -0.000000000000000000, -0.000000000000000000, 1.000000000000000000 ) ) ;
#10805=ORIENTED_EDGE ( 'NONE', *, *, #16810, .F. ) ;
#10821=ADVANCED_FACE ( 'NONE', ( #15307 ), #21183, .F. ) ;
#10822=VERTEX_POINT ( 'NONE', #19002 ) ;
#10827=DIRECTION ( 'NONE',  ( 1.000000000000000000, 0.000000000000000000, 0.000000000000000000 ) ) ;
#10832=VERTEX_POINT ( 'NONE', #13618 ) ;
#10839=AXIS2_PLACEMENT_3D ( 'NONE', #17592, #12227, #23241 ) ;
#10849=EDGE_LOOP ( 'NONE', ( #14000, #7483, #16350, #12107 ) ) ;
#10853=DIRECTION ( 'NONE',  ( 0.000000000000000000, 0.000000000000000000, 1.000000000000000000 ) ) ;
#10867=VERTEX_POINT ( 'NONE', #4849 ) ;
#10871=DIRECTION ( 'NONE',  ( 0.8571673007021120005, 1.049727191138618326E-16, -0.5150380749100547106 ) ) ;
#10872=PLANE ( 'NONE',  #2969 ) ;
#10877=ORIENTED_EDGE ( 'NONE', *, *, #20547, .F. ) ;
#10890=DIRECTION ( 'NONE',  ( -0.000000000000000000, -0.000000000000000000, -1.000000000000000000 ) ) ;
#10891=DIRECTION ( 'NONE',  ( -0.000000000000000000, -0.000000000000000000, -1.000000000000000000 ) ) ;
#10892=DIRECTION ( 'NONE',  ( 1.000000000000000000, 1.360567432138674546E-16, -0.000000000000000000 ) ) ;
#10893=CIRCLE ( 'NONE', #16737, 4.499999999999997335 ) ;
#10894=DIRECTION ( 'NONE',  ( -1.000000000000000000, 0.000000000000000000, 0.000000000000000000 ) ) ;
#10918=DIRECTION ( 'NONE',  ( 0.5579568342432823513, 0.8298699724180977899, 0.000000000000000000 ) ) ;
#10919=DIRECTION ( 'NONE',  ( -0.000000000000000000, 0.000000000000000000, -1.000000000000000000 ) ) ;
#10923=STYLED_ITEM('',(#24141),#18364);
#10933=DIRECTION ( 'NONE',  ( 0.000000000000000000, 0.000000000000000000, -1.000000000000000000 ) ) ;
#10942=EDGE_CURVE ( 'NONE', #13312, #12511, #16036, .T. ) ;
#10948=DIRECTION ( 'NONE',  ( 0.000000000000000000, 0.000000000000000000, 1.000000000000000000 ) ) ;
#10949=CARTESIAN_POINT ( 'NONE',  ( -28.99999999999999645, -29.50000000000000000, -3.000000000000000000 ) ) ;
#10955=CARTESIAN_POINT ( 'NONE',  ( 42.62132034355962418, -25.48082444701818616, 6.173874856195240421E-16 ) ) ;
#10966=DIRECTION ( 'NONE',  ( -0.000000000000000000, 1.000000000000000000, -0.000000000000000000 ) ) ;
#10967=DIRECTION ( 'NONE',  ( 0.000000000000000000, -0.000000000000000000, 1.000000000000000000 ) ) ;
#10976=AXIS2_PLACEMENT_3D ( 'NONE', #11725, #21283, #19201 ) ;
#10980=DIRECTION ( 'NONE',  ( 0.7052211081716905916, -0.7089874389501501506, -0.000000000000000000 ) ) ;
#10986=EDGE_LOOP ( 'NONE', ( #18299, #8222, #18728, #22021 ) ) ;
#10989=EDGE_LOOP ( 'NONE', ( #7638, #11181, #19852, #23262 ) ) ;
#10994=AXIS2_PLACEMENT_3D ( 'NONE', #18333, #7439, #7229 ) ;
#10996=VERTEX_POINT ( 'NONE', #9198 ) ;
#11004=CARTESIAN_POINT ( 'NONE',  ( 42.00000000000000000, 25.22443390181681266, -0.6213203435596420521 ) ) ;
#11032=DIRECTION ( 'NONE',  ( -0.000000000000000000, -0.000000000000000000, -1.000000000000000000 ) ) ;
#11035=CYLINDRICAL_SURFACE ( 'NONE', #11582, 10.00000000000000178 ) ;
#11036=DIRECTION ( 'NONE',  ( -0.000000000000000000, -0.000000000000000000, -1.000000000000000000 ) ) ;
#11041=AXIS2_PLACEMENT_3D ( 'NONE', #6053, #7982, #9570 ) ;
#11049=ORIENTED_EDGE ( 'NONE', *, *, #275, .F. ) ;
#11055=EDGE_CURVE ( 'NONE', #6327, #16103, #19161, .T. ) ;
#11056=DIRECTION ( 'NONE',  ( -1.000000000000000000, 0.000000000000000000, 0.000000000000000000 ) ) ;
#11062=DIRECTION ( 'NONE',  ( -0.000000000000000000, -0.000000000000000000, -1.000000000000000000 ) ) ;
#11067=DIRECTION ( 'NONE',  ( -0.000000000000000000, -0.000000000000000000, -1.000000000000000000 ) ) ;
#11072=CARTESIAN_POINT ( 'NONE',  ( -28.99999999999999645, 29.50000000000000000, -2.224999999999995204 ) ) ;
#11076=VECTOR ( 'NONE', #14172, 1000.000000000000000 ) ;
#11081=AXIS2_PLACEMENT_3D ( 'NONE', #8859, #5202, #12865 ) ;
#11082=AXIS2_PLACEMENT_3D ( 'NONE', #23035, #830, #19977 ) ;
#11083=CARTESIAN_POINT ( 'NONE',  ( -40.66734255040736201, -26.56420859267092283, -1.500000000000000000 ) ) ;
#11086=ADVANCED_FACE ( 'NONE', ( #20425 ), #12522, .F. ) ;
#11093=ORIENTED_EDGE ( 'NONE', *, *, #20615, .F. ) ;
#11096=VECTOR ( 'NONE', #5430, 1000.000000000000000 ) ;
#11098=DIRECTION ( 'NONE',  ( 0.000000000000000000, 0.000000000000000000, 1.000000000000000000 ) ) ;
#11110=AXIS2_PLACEMENT_3D ( 'NONE', #9031, #15196, #16481 ) ;
#11120=ORIENTED_EDGE ( 'NONE', *, *, #1162, .T. ) ;
#11126=CARTESIAN_POINT ( 'NONE',  ( 30.16774287754691386, -40.66994976491903913, -3.000000000000000000 ) ) ;
#11131=FACE_BOUND ( 'NONE', #7741, .T. ) ;
#11135=CARTESIAN_POINT ( 'NONE',  ( -30.16774287754692807, 40.66994976491904623, -1.500000000000000000 ) ) ;
#11136=DIRECTION ( 'NONE',  ( 0.000000000000000000, 0.000000000000000000, 1.000000000000000000 ) ) ;
#11142=EDGE_CURVE ( 'NONE', #5523, #5799, #16868, .T. ) ;
#11150=DIRECTION ( 'NONE',  ( 0.000000000000000000, -0.000000000000000000, 1.000000000000000000 ) ) ;
#11154=ORIENTED_EDGE ( 'NONE', *, *, #12904, .T. ) ;
#11164=EDGE_CURVE ( 'NONE', #7451, #2444, #22509, .T. ) ;
#11173=VERTEX_POINT ( 'NONE', #187 ) ;
#11181=ORIENTED_EDGE ( 'NONE', *, *, #5495, .F. ) ;
#11193=CARTESIAN_POINT ( 'NONE',  ( 0.000000000000000000, -45.00000000000000000, -3.000000000000000000 ) ) ;
#11199=CARTESIAN_POINT ( 'NONE',  ( -41.99999999999997158, -25.22443390181683043, -3.000000000000000000 ) ) ;
#11202=CARTESIAN_POINT ( 'NONE',  ( 0.000000000000000000, 45.00000000000000000, -3.000000000000000000 ) ) ;
#11214=EDGE_CURVE ( 'NONE', #20840, #16760, #21894, .T. ) ;
#11226=ORIENTED_EDGE ( 'NONE', *, *, #16810, .T. ) ;
#11227=VERTEX_POINT ( 'NONE', #22875 ) ;
#11234=DIRECTION ( 'NONE',  ( 1.000000000000000000, 0.000000000000000000, 0.000000000000000000 ) ) ;
#11241=DIRECTION ( 'NONE',  ( -0.000000000000000000, -0.000000000000000000, -1.000000000000000000 ) ) ;
#11243=DIRECTION ( 'NONE',  ( 0.000000000000000000, 0.000000000000000000, -1.000000000000000000 ) ) ;
#11244=DIRECTION ( 'NONE',  ( -1.000000000000000000, 0.000000000000000000, 0.000000000000000000 ) ) ;
#11252=EDGE_LOOP ( 'NONE', ( #9218, #14747, #20299, #8511 ) ) ;
#11255=ORIENTED_EDGE ( 'NONE', *, *, #14299, .F. ) ;
#11257=DIRECTION ( 'NONE',  ( -1.000000000000000000, 0.000000000000000000, 0.000000000000000000 ) ) ;
#11267=EDGE_LOOP ( 'NONE', ( #6104, #6192, #20264, #13318 ) ) ;
#11280=ORIENTED_EDGE ( 'NONE', *, *, #9348, .F. ) ;
#11283=AXIS2_PLACEMENT_3D ( 'NONE', #15500, #17712, #10121 ) ;
#11300=( GEOMETRIC_REPRESENTATION_CONTEXT ( 3 ) GLOBAL_UNCERTAINTY_ASSIGNED_CONTEXT ( ( #13754 ) ) GLOBAL_UNIT_ASSIGNED_CONTEXT ( ( #11770, #104, #5820 ) ) REPRESENTATION_CONTEXT ( 'NONE', 'WORKASPACE' ) );
#11306=CARTESIAN_POINT ( 'NONE',  ( 3.890962118697714531E-15, 15.50000000000000000, -2.999999999999999112 ) ) ;
#11315=AXIS2_PLACEMENT_3D ( 'NONE', #20094, #16657, #12982 ) ;
#11319=EDGE_LOOP ( 'NONE', ( #109, #14937 ) ) ;
#11333=EDGE_CURVE ( 'NONE', #6140, #21092, #11747, .T. ) ;
#11340=DIRECTION ( 'NONE',  ( 1.000000000000000000, 0.000000000000000000, -0.000000000000000000 ) ) ;
#11343=CARTESIAN_POINT ( 'NONE',  ( 3.890962118697714531E-15, 15.50000000000000000, -40.80000000000000426 ) ) ;
#11344=ORIENTED_EDGE ( 'NONE', *, *, #21075, .F. ) ;
#11346=EDGE_LOOP ( 'NONE', ( #16564, #14201, #10346, #6269 ) ) ;
#11352=AXIS2_PLACEMENT_3D ( 'NONE', #16747, #1647, #9199 ) ;
#11357=( BOUNDED_CURVE ( )  B_SPLINE_CURVE ( 3, ( #20269, #10955, #18432, #19912 ),
 .UNSPECIFIED., .F., .T. ) 
 B_SPLINE_CURVE_WITH_KNOTS ( ( 4, 4 ),
 ( 1.570796326794895670, 3.141592653589793116 ),
 .UNSPECIFIED. ) 
 CURVE ( )  GEOMETRIC_REPRESENTATION_ITEM ( )  RATIONAL_B_SPLINE_CURVE ( ( 1.000000000000000000, 0.8047378541243648264, 0.8047378541243648264, 1.000000000000000000 ) ) 
 REPRESENTATION_ITEM ( '' )  );
#11360=ORIENTED_EDGE ( 'NONE', *, *, #15527, .T. ) ;
#11368=ORIENTED_EDGE ( 'NONE', *, *, #19910, .F. ) ;
#11374=VECTOR ( 'NONE', #1568, 1000.000000000000000 ) ;
#11392=LINE ( 'NONE', #23013, #2064 ) ;
#11397=CIRCLE ( 'NONE', #511, 8.999999999999998224 ) ;
#11402=FACE_OUTER_BOUND ( 'NONE', #8903, .T. ) ;
#11404=AXIS2_PLACEMENT_3D ( 'NONE', #665, #22552, #5833 ) ;
#11415=ADVANCED_FACE ( 'NONE', ( #13283 ), #11449, .F. ) ;
#11416=AXIS2_PLACEMENT_3D ( 'NONE', #19578, #4587, #2856 ) ;
#11419=CARTESIAN_POINT ( 'NONE',  ( 40.23082370883257397, -27.62204025492844650, -3.000000000000000000 ) ) ;
#11425=ORIENTED_EDGE ( 'NONE', *, *, #7082, .T. ) ;
#11428=CARTESIAN_POINT ( 'NONE',  ( -36.00000000000001421, 50.99999999999999289, 12.50000000000000000 ) ) ;
#11430=DIRECTION ( 'NONE',  ( -5.501724186093585079E-16, -1.000000000000000000, 0.000000000000000000 ) ) ;
#11432=AXIS2_PLACEMENT_3D ( 'NONE', #3655, #11067, #16704 ) ;
#11433=ORIENTED_EDGE ( 'NONE', *, *, #17384, .T. ) ;
#11435=AXIS2_PLACEMENT_3D ( 'NONE', #11679, #9728, #13545 ) ;
#11436=VERTEX_POINT ( 'NONE', #6108 ) ;
#11439=VECTOR ( 'NONE', #163, 1000.000000000000000 ) ;
#11449=CYLINDRICAL_SURFACE ( 'NONE', #9027, 4.499999999999997335 ) ;
#11460=CIRCLE ( 'NONE', #6039, 15.00000000000000000 ) ;
#11462=CARTESIAN_POINT ( 'NONE',  ( 10.00000000000000533, 15.50000000000000000, -40.80000000000000426 ) ) ;
#11465=DIRECTION ( 'NONE',  ( -0.000000000000000000, -0.000000000000000000, -1.000000000000000000 ) ) ;
#11466=DIRECTION ( 'NONE',  ( -0.000000000000000000, -0.000000000000000000, -1.000000000000000000 ) ) ;
#11476=ADVANCED_FACE ( 'NONE', ( #4036 ), #743, .F. ) ;
#11488=ORIENTED_EDGE ( 'NONE', *, *, #3971, .F. ) ;
#11491=EDGE_LOOP ( 'NONE', ( #14425, #14582, #17067, #15241 ) ) ;
#11498=CARTESIAN_POINT ( 'NONE',  ( 24.75000000000000711, 29.50000000000000000, 14.00000000000000178 ) ) ;
#11499=VERTEX_POINT ( 'NONE', #7785 ) ;
#11500=CARTESIAN_POINT ( 'NONE',  ( 35.99999999999999289, -51.00000000000000711, 12.50000000000000000 ) ) ;
#11502=DIRECTION ( 'NONE',  ( -0.7089874389501490404, -0.7052211081716915908, 0.000000000000000000 ) ) ;
#11505=VERTEX_POINT ( 'NONE', #15485 ) ;
#11508=ORIENTED_EDGE ( 'NONE', *, *, #20243, .F. ) ;
#11513=ORIENTED_EDGE ( 'NONE', *, *, #5020, .F. ) ;
#11521=DIRECTION ( 'NONE',  ( 0.7071067811865474617, 8.659560562354932858E-17, -0.7071067811865474617 ) ) ;
#11522=FACE_OUTER_BOUND ( 'NONE', #20242, .T. ) ;
#11532=FACE_OUTER_BOUND ( 'NONE', #7607, .T. ) ;
#11534=EDGE_CURVE ( 'NONE', #14876, #17470, #19967, .T. ) ;
#11541=ORIENTED_EDGE ( 'NONE', *, *, #3298, .F. ) ;
#11546=CIRCLE ( 'NONE', #1063, 8.999999999999998224 ) ;
#11547=ORIENTED_EDGE ( 'NONE', *, *, #12970, .T. ) ;
#11550=AXIS2_PLACEMENT_3D ( 'NONE', #19841, #3110, #5068 ) ;
#11553=CARTESIAN_POINT ( 'NONE',  ( 43.49999999999997868, -25.84341543330623381, 0.000000000000000000 ) ) ;
#11557=DIRECTION ( 'NONE',  ( -0.000000000000000000, -0.000000000000000000, -1.000000000000000000 ) ) ;
#11567=LINE ( 'NONE', #7017, #22825 ) ;
#11574=DIRECTION ( 'NONE',  ( -0.000000000000000000, -0.000000000000000000, -1.000000000000000000 ) ) ;
#11582=AXIS2_PLACEMENT_3D ( 'NONE', #5564, #10804, #8750 ) ;
#11588=EDGE_CURVE ( 'NONE', #2444, #19429, #23562, .T. ) ;
#11609=LINE ( 'NONE', #11126, #13167 ) ;
#11614=DIRECTION ( 'NONE',  ( 1.000000000000000000, 0.000000000000000000, 0.000000000000000000 ) ) ;
#11618=EDGE_LOOP ( 'NONE', ( #16516, #20680, #23343 ) ) ;
#11619=CYLINDRICAL_SURFACE ( 'NONE', #21189, 15.00000000000000000 ) ;
#11620=DIRECTION ( 'NONE',  ( 1.360567432138674300E-16, -1.000000000000000000, 0.000000000000000000 ) ) ;
#11624=ORIENTED_EDGE ( 'NONE', *, *, #23788, .T. ) ;
#11629=LINE ( 'NONE', #19100, #20769 ) ;
#11633=CARTESIAN_POINT ( 'NONE',  ( -23.97499999999999787, -29.50000000000000000, -3.000000000000000000 ) ) ;
#11637=EDGE_CURVE ( 'NONE', #12712, #1878, #2841, .T. ) ;
#11639=CARTESIAN_POINT ( 'NONE',  ( -28.99999999999999645, 29.50000000000000000, 14.00000000000000178 ) ) ;
#11640=DIRECTION ( 'NONE',  ( -1.000000000000000000, 0.000000000000000000, 0.000000000000000000 ) ) ;
#11647=AXIS2_PLACEMENT_3D ( 'NONE', #21677, #21792, #16522 ) ;
#11654=CARTESIAN_POINT ( 'NONE',  ( -1.999999999999996669, -45.00000000000000000, -3.000000000000000000 ) ) ;
#11661=EDGE_CURVE ( 'NONE', #10567, #12610, #14381, .T. ) ;
#11665=DIRECTION ( 'NONE',  ( -1.000000000000000000, 0.000000000000000000, 0.000000000000000000 ) ) ;
#11669=DIRECTION ( 'NONE',  ( -1.000000000000000000, 0.000000000000000000, 0.000000000000000000 ) ) ;
#11672=ORIENTED_EDGE ( 'NONE', *, *, #13482, .F. ) ;
#11675=CIRCLE ( 'NONE', #2358, 4.249999999999993783 ) ;
#11679=CARTESIAN_POINT ( 'NONE',  ( -41.73082370883257397, -27.62204025492846071, -1.500000000000000000 ) ) ;
#11682=DIRECTION ( 'NONE',  ( 0.000000000000000000, -0.000000000000000000, 1.000000000000000000 ) ) ;
#11697=PLANE ( 'NONE',  #16348 ) ;
#11702=ORIENTED_EDGE ( 'NONE', *, *, #3862, .T. ) ;
#11706=CARTESIAN_POINT ( 'NONE',  ( 0.000000000000000000, -45.00000000000000000, -8.673617379884035472E-16 ) ) ;
#11708=DIRECTION ( 'NONE',  ( -0.000000000000000000, -0.000000000000000000, -1.000000000000000000 ) ) ;
#11713=CARTESIAN_POINT ( 'NONE',  ( 28.99999999999999645, 29.49999999999999645, -1.500000000000000000 ) ) ;
#11717=CARTESIAN_POINT ( 'NONE',  ( -40.50000000000000711, 50.99999999999999289, 0.5000000000000004441 ) ) ;
#11720=VERTEX_POINT ( 'NONE', #7303 ) ;
#11725=CARTESIAN_POINT ( 'NONE',  ( -35.99999999999995026, 59.99999999999998579, 12.50000000000000000 ) ) ;
#11728=CARTESIAN_POINT ( 'NONE',  ( -41.73082370883260239, 27.62204025492845361, -1.500000000000000000 ) ) ;
#11730=DIRECTION ( 'NONE',  ( -1.000000000000000000, 0.000000000000000000, 0.000000000000000000 ) ) ;
#11731=DIRECTION ( 'NONE',  ( -0.000000000000000000, -0.000000000000000000, -1.000000000000000000 ) ) ;
#11736=EDGE_CURVE ( 'NONE', #15766, #5717, #4795, .T. ) ;
#11743=AXIS2_PLACEMENT_3D ( 'NONE', #23564, #12321, #19668 ) ;
#11747=CIRCLE ( 'NONE', #2418, 12.73082370883260594 ) ;
#11749=CARTESIAN_POINT ( 'NONE',  ( 30.32370777929697780, -42.16181938034193877, -1.500000000000000000 ) ) ;
#11751=DIRECTION ( 'NONE',  ( -0.000000000000000000, -0.000000000000000000, -1.000000000000000000 ) ) ;
#11754=DIRECTION ( 'NONE',  ( -1.000000000000000000, 0.000000000000000000, 0.000000000000000000 ) ) ;
#11755=CYLINDRICAL_SURFACE ( 'NONE', #21422, 1.500000000000000000 ) ;
#11756=EDGE_LOOP ( 'NONE', ( #5502, #169, #860, #18822 ) ) ;
#11757=CARTESIAN_POINT ( 'NONE',  ( -41.73082370883257397, -29.50000000000000711, -1.500000000000000000 ) ) ;
#11759=ORIENTED_EDGE ( 'NONE', *, *, #14404, .T. ) ;
#11760=DIRECTION ( 'NONE',  ( -0.000000000000000000, -0.000000000000000000, 1.000000000000000000 ) ) ;
#11767=EDGE_CURVE ( 'NONE', #15771, #3651, #10610, .T. ) ;
#11770=( LENGTH_UNIT ( ) NAMED_UNIT ( * ) SI_UNIT ( .MILLI., .METRE. ) );
#11772=ORIENTED_EDGE ( 'NONE', *, *, #4675, .T. ) ;
#11778=DIRECTION ( 'NONE',  ( 1.000000000000000000, 0.000000000000000000, 0.000000000000000000 ) ) ;
#11812=CARTESIAN_POINT ( 'NONE',  ( -14.99999999999999645, 15.50000000000000178, 7.700000000000001954 ) ) ;
#11818=DIRECTION ( 'NONE',  ( 0.000000000000000000, 0.000000000000000000, -1.000000000000000000 ) ) ;
#11829=VECTOR ( 'NONE', #11838, 1000.000000000000000 ) ;
#11838=DIRECTION ( 'NONE',  ( 0.000000000000000000, 1.000000000000000000, 0.000000000000000000 ) ) ;
#11840=ORIENTED_EDGE ( 'NONE', *, *, #5845, .T. ) ;
#11844=ADVANCED_FACE ( 'NONE', ( #18408 ), #7057, .F. ) ;
#11847=ORIENTED_EDGE ( 'NONE', *, *, #23057, .T. ) ;
#11858=CARTESIAN_POINT ( 'NONE',  ( -2.024999999999999911, 45.00000000000000000, -3.000000000000000000 ) ) ;
#11859=AXIS2_PLACEMENT_3D ( 'NONE', #20324, #18373, #1668 ) ;
#11864=CARTESIAN_POINT ( 'NONE',  ( 3.890962118697714531E-15, 15.50000000000000000, 19.70000000000000284 ) ) ;
#11866=AXIS2_PLACEMENT_3D ( 'NONE', #11728, #19574, #19341 ) ;
#11878=ORIENTED_EDGE ( 'NONE', *, *, #9412, .T. ) ;
#11883=CARTESIAN_POINT ( 'NONE',  ( -23.97499999999999787, 29.50000000000000000, -3.000000000000000000 ) ) ;
#11887=DIRECTION ( 'NONE',  ( 0.000000000000000000, 0.000000000000000000, -1.000000000000000000 ) ) ;
#11893=LINE ( 'NONE', #17999, #23904 ) ;
#11895=ORIENTED_EDGE ( 'NONE', *, *, #20043, .T. ) ;
#11897=CARTESIAN_POINT ( 'NONE',  ( 35.99999999999999289, 50.99999999999999289, 0.5000000000000000000 ) ) ;
#11909=AXIS2_PLACEMENT_3D ( 'NONE', #19781, #16328, #16571 ) ;
#11920=CARTESIAN_POINT ( 'NONE',  ( 0.000000000000000000, 15.50000000000000000, 7.700000000000001954 ) ) ;
#11926=FACE_OUTER_BOUND ( 'NONE', #21088, .T. ) ;
#11927=CARTESIAN_POINT ( 'NONE',  ( 35.99999999999999289, -51.00000000000000711, 0.000000000000000000 ) ) ;
#11938=ORIENTED_EDGE ( 'NONE', *, *, #20164, .F. ) ;
#11947=EDGE_LOOP ( 'NONE', ( #8072, #4322 ) ) ;
#11954=LINE ( 'NONE', #19422, #7936 ) ;
#11956=ORIENTED_EDGE ( 'NONE', *, *, #20164, .T. ) ;
#11958=DIRECTION ( 'NONE',  ( 0.000000000000000000, 1.000000000000000000, 0.000000000000000000 ) ) ;
#11966=ORIENTED_EDGE ( 'NONE', *, *, #12674, .F. ) ;
#11975=CARTESIAN_POINT ( 'NONE',  ( 0.000000000000000000, 32.75000000000000000, 16.70000000000000284 ) ) ;
#11978=CARTESIAN_POINT ( 'NONE',  ( 28.99999999999999645, 29.49999999999999645, 0.000000000000000000 ) ) ;
#11979=DIRECTION ( 'NONE',  ( -0.000000000000000000, 0.000000000000000000, -1.000000000000000000 ) ) ;
#11999=ORIENTED_EDGE ( 'NONE', *, *, #9412, .F. ) ;
#12005=CARTESIAN_POINT ( 'NONE',  ( -28.99999999999999645, 29.50000000000000000, 14.00000000000000178 ) ) ;
#12006=ORIENTED_EDGE ( 'NONE', *, *, #17441, .T. ) ;
#12010=LINE ( 'NONE', #4607, #22203 ) ;
#12022=ORIENTED_EDGE ( 'NONE', *, *, #17522, .T. ) ;
#12028=AXIS2_PLACEMENT_3D ( 'NONE', #15691, #10070, #2654 ) ;
#12031=CARTESIAN_POINT ( 'NONE',  ( 15.00000000000000355, 15.50000000000000000, 16.70000000000000284 ) ) ;
#12039=DIRECTION ( 'NONE',  ( -1.000000000000000000, 0.000000000000000000, 0.000000000000000000 ) ) ;
#12062=DIRECTION ( 'NONE',  ( 0.000000000000000000, 0.000000000000000000, 1.000000000000000000 ) ) ;
#12068=CARTESIAN_POINT ( 'NONE',  ( 3.890962118697714531E-15, 15.50000000000000000, 7.700000000000001954 ) ) ;
#12075=FACE_OUTER_BOUND ( 'NONE', #11947, .T. ) ;
#12087=FACE_OUTER_BOUND ( 'NONE', #18668, .T. ) ;
#12089=CARTESIAN_POINT ( 'NONE',  ( -42.00000000000000000, 25.22443390181683043, -1.500000000000000000 ) ) ;
#12105=VERTEX_POINT ( 'NONE', #14429 ) ;
#12107=ORIENTED_EDGE ( 'NONE', *, *, #14116, .T. ) ;
#12128=CARTESIAN_POINT ( 'NONE',  ( -17.25000000000000000, 15.50000000000000000, 16.70000000000000284 ) ) ;
#12129=EDGE_CURVE ( 'NONE', #10256, #18213, #12579, .T. ) ;
#12130=FACE_OUTER_BOUND ( 'NONE', #11491, .T. ) ;
#12142=VERTEX_POINT ( 'NONE', #17883 ) ;
#12152=CARTESIAN_POINT ( 'NONE',  ( 0.000000000000000000, -45.00000000000000000, -3.000000000000000000 ) ) ;
#12161=DIRECTION ( 'NONE',  ( -0.000000000000000000, -0.000000000000000000, 1.000000000000000000 ) ) ;
#12173=EDGE_CURVE ( 'NONE', #1863, #8263, #23836, .T. ) ;
#12190=DIRECTION ( 'NONE',  ( 1.000000000000000000, 0.000000000000000000, 0.000000000000000000 ) ) ;
#12205=VERTEX_POINT ( 'NONE', #9654 ) ;
#12211=CARTESIAN_POINT ( 'NONE',  ( -1.029124893018731811E-15, -45.00000000000000000, 1.201721238055119212 ) ) ;
#12227=DIRECTION ( 'NONE',  ( -0.000000000000000000, -0.000000000000000000, -1.000000000000000000 ) ) ;
#12229=EDGE_CURVE ( 'NONE', #16185, #17812, #11397, .T. ) ;
#12230=VERTEX_POINT ( 'NONE', #7704 ) ;
#12232=DIRECTION ( 'NONE',  ( -1.000000000000000000, -8.175701033892699531E-16, 0.000000000000000000 ) ) ;
#12246=ORIENTED_EDGE ( 'NONE', *, *, #2709, .T. ) ;
#12248=EDGE_LOOP ( 'NONE', ( #4162, #19194, #22627, #10182 ) ) ;
#12251=DIRECTION ( 'NONE',  ( -0.000000000000000000, -0.000000000000000000, -1.000000000000000000 ) ) ;
#12286=DIRECTION ( 'NONE',  ( -0.000000000000000000, -0.000000000000000000, -1.000000000000000000 ) ) ;
#12289=ORIENTED_EDGE ( 'NONE', *, *, #22772, .T. ) ;
#12291=LINE ( 'NONE', #8512, #3999 ) ;
#12295=CARTESIAN_POINT ( 'NONE',  ( -45.00000000000000000, -50.99999999999993605, 0.000000000000000000 ) ) ;
#12303=EDGE_LOOP ( 'NONE', ( #17905, #13581, #11759, #14792 ) ) ;
#12307=ORIENTED_EDGE ( 'NONE', *, *, #19908, .F. ) ;
#12309=AXIS2_PLACEMENT_3D ( 'NONE', #6264, #23481, #6531 ) ;
#12321=DIRECTION ( 'NONE',  ( -0.000000000000000000, -0.000000000000000000, -1.000000000000000000 ) ) ;
#12323=ADVANCED_FACE ( 'NONE', ( #2233 ), #20417, .F. ) ;
#12332=ORIENTED_EDGE ( 'NONE', *, *, #18094, .F. ) ;
#12371=EDGE_CURVE ( 'NONE', #16325, #15649, #21558, .T. ) ;
#12390=EDGE_LOOP ( 'NONE', ( #5977, #11360, #5768, #464 ) ) ;
#12402=AXIS2_PLACEMENT_3D ( 'NONE', #18831, #9543, #3714 ) ;
#12407=LINE ( 'NONE', #6456, #17248 ) ;
#12408=CARTESIAN_POINT ( 'NONE',  ( -36.00000000000000711, -51.00000000000000711, 0.5000000000000004441 ) ) ;
#12424=DIRECTION ( 'NONE',  ( 0.000000000000000000, 0.000000000000000000, 1.000000000000000000 ) ) ;
#12425=CARTESIAN_POINT ( 'NONE',  ( 3.890962118697714531E-15, 15.50000000000000000, 19.70000000000000284 ) ) ;
#12429=EDGE_CURVE ( 'NONE', #3651, #3029, #14917, .T. ) ;
#12448=EDGE_CURVE ( 'NONE', #21069, #4705, #189, .T. ) ;
#12451=DIRECTION ( 'NONE',  ( -0.000000000000000000, -0.000000000000000000, -1.000000000000000000 ) ) ;
#12460=EDGE_LOOP ( 'NONE', ( #20153, #13978, #23924 ) ) ;
#12469=DIRECTION ( 'NONE',  ( -0.000000000000000000, -0.000000000000000000, 1.000000000000000000 ) ) ;
#12473=VECTOR ( 'NONE', #10980, 999.9999999999998863 ) ;
#12477=ORIENTED_EDGE ( 'NONE', *, *, #24078, .F. ) ;
#12479=ORIENTED_EDGE ( 'NONE', *, *, #2401, .T. ) ;
#12483=ORIENTED_EDGE ( 'NONE', *, *, #16306, .T. ) ;
#12497=ORIENTED_EDGE ( 'NONE', *, *, #3886, .F. ) ;
#12504=AXIS2_PLACEMENT_3D ( 'NONE', #11897, #7994, #13370 ) ;
#12511=VERTEX_POINT ( 'NONE', #19573 ) ;
#12521=CIRCLE ( 'NONE', #2006, 1.499999999999994449 ) ;
#12522=TOROIDAL_SURFACE ( 'NONE', #14855, 12.73082370883259706, 1.500000000000000000 ) ;
#12524=VERTEX_POINT ( 'NONE', #19822 ) ;
#12526=ORIENTED_EDGE ( 'NONE', *, *, #5918, .F. ) ;
#12534=DIRECTION ( 'NONE',  ( -1.000000000000000000, 0.000000000000000000, 0.000000000000000000 ) ) ;
#12537=CIRCLE ( 'NONE', #13714, 1.500000000000000000 ) ;
#12549=EDGE_CURVE ( 'NONE', #22890, #16185, #19338, .T. ) ;
#12576=DIRECTION ( 'NONE',  ( 0.7052211081716914798, -0.7089874389501492624, 0.000000000000000000 ) ) ;
#12578=CARTESIAN_POINT ( 'NONE',  ( -30.68762588338048403, 45.64284848299540442, -1.500000000000000000 ) ) ;
#12579=CIRCLE ( 'NONE', #14907, 3.500000000000003109 ) ;
#12583=ADVANCED_FACE ( 'NONE', ( #13700 ), #4834, .T. ) ;
#12584=ORIENTED_EDGE ( 'NONE', *, *, #9757, .F. ) ;
#12593=CARTESIAN_POINT ( 'NONE',  ( 40.23082370883257397, -27.62204025492844650, -1.500000000000000000 ) ) ;
#12597=ORIENTED_EDGE ( 'NONE', *, *, #3886, .T. ) ;
#12602=AXIS2_PLACEMENT_3D ( 'NONE', #21795, #10668, #18139 ) ;
#12610=VERTEX_POINT ( 'NONE', #23108 ) ;
#12611=CARTESIAN_POINT ( 'NONE',  ( 0.000000000000000000, 45.00000000000000000, -2.974999999999996092 ) ) ;
#12613=DIRECTION ( 'NONE',  ( -1.000000000000000000, 0.000000000000000000, 0.000000000000000000 ) ) ;
#12616=EDGE_CURVE ( 'NONE', #20236, #18123, #22356, .T. ) ;
#12619=CARTESIAN_POINT ( 'NONE',  ( -28.99999999999998579, -29.50000000000000711, -1.500000000000000000 ) ) ;
#12630=AXIS2_PLACEMENT_3D ( 'NONE', #10464, #21713, #12039 ) ;
#12639=DIRECTION ( 'NONE',  ( -0.000000000000000000, -0.000000000000000000, -1.000000000000000000 ) ) ;
#12642=DIRECTION ( 'NONE',  ( -1.000000000000000000, -4.625929269271481378E-15, 0.000000000000000000 ) ) ;
#12650=DIRECTION ( 'NONE',  ( -5.501724186093582121E-16, 1.000000000000000000, -0.000000000000000000 ) ) ;
#12653=CARTESIAN_POINT ( 'NONE',  ( 0.000000000000000000, -45.00000000000000000, -3.000000000000000000 ) ) ;
#12654=ORIENTED_EDGE ( 'NONE', *, *, #8113, .T. ) ;
#12662=VERTEX_POINT ( 'NONE', #19706 ) ;
#12670=CONICAL_SURFACE ( 'NONE', #13066, 2.024999999999999911, 0.7853981633974222998 ) ;
#12674=EDGE_CURVE ( 'NONE', #14048, #22424, #15721, .T. ) ;
#12691=DIRECTION ( 'NONE',  ( -0.000000000000000000, -0.000000000000000000, -1.000000000000000000 ) ) ;
#12696=DIRECTION ( 'NONE',  ( -1.000000000000000000, 0.000000000000000000, 0.000000000000000000 ) ) ;
#12712=VERTEX_POINT ( 'NONE', #16619 ) ;
#12713=VECTOR ( 'NONE', #15131, 999.9999999999998863 ) ;
#12724=EDGE_LOOP ( 'NONE', ( #14180, #20532, #11702, #22237 ) ) ;
#12726=EDGE_CURVE ( 'NONE', #3029, #13623, #9854, .T. ) ;
#12733=CARTESIAN_POINT ( 'NONE',  ( -42.00000000000000000, 25.22443390181682688, -0.6213203435596427182 ) ) ;
#12740=DIRECTION ( 'NONE',  ( -0.000000000000000000, -0.000000000000000000, 1.000000000000000000 ) ) ;
#12744=CARTESIAN_POINT ( 'NONE',  ( -30.68762588338048403, 45.64284848299540442, -3.000000000000000000 ) ) ;
#12756=LINE ( 'NONE', #7273, #22406 ) ;
#12759=AXIS2_PLACEMENT_3D ( 'NONE', #23239, #4685, #21511 ) ;
#12762=DIRECTION ( 'NONE',  ( -1.000000000000000000, 0.000000000000000000, 0.000000000000000000 ) ) ;
#12764=EDGE_LOOP ( 'NONE', ( #22788, #631, #7744, #4614 ) ) ;
#12767=ORIENTED_EDGE ( 'NONE', *, *, #7246, .T. ) ;
#12781=ORIENTED_EDGE ( 'NONE', *, *, #22971, .F. ) ;
#12783=ORIENTED_EDGE ( 'NONE', *, *, #4941, .T. ) ;
#12795=CARTESIAN_POINT ( 'NONE',  ( 3.890962118697714531E-15, 15.50000000000000000, 16.70000000000000284 ) ) ;
#12812=EDGE_CURVE ( 'NONE', #15518, #7322, #1346, .T. ) ;
#12821=AXIS2_PLACEMENT_3D ( 'NONE', #5590, #16792, #458 ) ;
#12825=ADVANCED_FACE ( 'NONE', ( #3921 ), #2495, .F. ) ;
#12850=DIRECTION ( 'NONE',  ( -1.000000000000000000, 0.000000000000000000, 0.000000000000000000 ) ) ;
#12854=CARTESIAN_POINT ( 'NONE',  ( 40.66734255040738333, 26.56420859267091217, -3.000000000000000000 ) ) ;
#12857=ORIENTED_EDGE ( 'NONE', *, *, #20803, .F. ) ;
#12863=ORIENTED_EDGE ( 'NONE', *, *, #20385, .T. ) ;
#12865=DIRECTION ( 'NONE',  ( -1.000000000000000000, 0.000000000000000000, 0.000000000000000000 ) ) ;
#12868=ORIENTED_EDGE ( 'NONE', *, *, #3971, .T. ) ;
#12888=ADVANCED_FACE ( 'NONE', ( #10381 ), #21619, .F. ) ;
#12892=AXIS2_PLACEMENT_3D ( 'NONE', #20235, #9591, #337 ) ;
#12894=EDGE_LOOP ( 'NONE', ( #7380, #16592, #20409, #1173 ) ) ;
#12898=CARTESIAN_POINT ( 'NONE',  ( -45.00000000000001421, 50.99999999999992184, 0.000000000000000000 ) ) ;
#12904=EDGE_CURVE ( 'NONE', #20508, #9321, #8051, .T. ) ;
#12910=CARTESIAN_POINT ( 'NONE',  ( 35.99999999999999289, -51.00000000000000711, 12.50000000000000000 ) ) ;
#12927=AXIS2_PLACEMENT_3D ( 'NONE', #10237, #17693, #8420 ) ;
#12928=CARTESIAN_POINT ( 'NONE',  ( 0.000000000000000000, 45.00000000000000000, -3.000000000000000000 ) ) ;
#12939=ORIENTED_EDGE ( 'NONE', *, *, #4161, .F. ) ;
#12942=AXIS2_PLACEMENT_3D ( 'NONE', #18543, #22095, #9247 ) ;
#12943=DIRECTION ( 'NONE',  ( -0.000000000000000000, -0.000000000000000000, -1.000000000000000000 ) ) ;
#12947=AXIS2_PLACEMENT_3D ( 'NONE', #5292, #23611, #23480 ) ;
#12961=AXIS2_PLACEMENT_3D ( 'NONE', #15149, #11243, #20793 ) ;
#12966=FACE_OUTER_BOUND ( 'NONE', #10989, .T. ) ;
#12970=EDGE_CURVE ( 'NONE', #12205, #10649, #4919, .T. ) ;
#12972=FACE_BOUND ( 'NONE', #1058, .T. ) ;
#12982=DIRECTION ( 'NONE',  ( -1.000000000000000000, 0.000000000000000000, 0.000000000000000000 ) ) ;
#12985=CONICAL_SURFACE ( 'NONE', #13376, 5.025000000000002132, 0.7853981633974482790 ) ;
#12986=AXIS2_PLACEMENT_3D ( 'NONE', #11500, #9667, #14920 ) ;
#12988=VERTEX_POINT ( 'NONE', #6363 ) ;
#12999=AXIS2_PLACEMENT_3D ( 'NONE', #15124, #18940, #17203 ) ;
#13012=DIRECTION ( 'NONE',  ( -0.000000000000000000, -0.000000000000000000, -1.000000000000000000 ) ) ;
#13025=EDGE_CURVE ( 'NONE', #17812, #14877, #10730, .T. ) ;
#13052=CARTESIAN_POINT ( 'NONE',  ( 0.000000000000000000, 15.50000000000000000, 14.70000000000000284 ) ) ;
#13066=AXIS2_PLACEMENT_3D ( 'NONE', #11193, #3896, #3659 ) ;
#13076=AXIS2_PLACEMENT_3D ( 'NONE', #22201, #9345, #3770 ) ;
#13091=CARTESIAN_POINT ( 'NONE',  ( -28.73477696352898292, 42.73830357953205805, -1.500000000000000000 ) ) ;
#13099=CARTESIAN_POINT ( 'NONE',  ( -33.24999999999999289, -29.50000000000000000, -3.000000000000000000 ) ) ;
#13100=CARTESIAN_POINT ( 'NONE',  ( 44.99999999999998579, 50.99999999999992184, 12.50000000000000000 ) ) ;
#13105=EDGE_CURVE ( 'NONE', #20508, #10567, #4118, .T. ) ;
#13109=VERTEX_POINT ( 'NONE', #7316 ) ;
#13127=VERTEX_POINT ( 'NONE', #14504 ) ;
#13142=CARTESIAN_POINT ( 'NONE',  ( 43.99999999999999289, -51.00000000000000711, 0.5000000000000000000 ) ) ;
#13150=CARTESIAN_POINT ( 'NONE',  ( -28.99999999999999645, 29.50000000000000000, -3.000000000000000000 ) ) ;
#13154=CIRCLE ( 'NONE', #15101, 5.000000000000004441 ) ;
#13159=EDGE_CURVE ( 'NONE', #5970, #19012, #21661, .T. ) ;
#13167=VECTOR ( 'NONE', #1985, 1000.000000000000000 ) ;
#13174=ORIENTED_EDGE ( 'NONE', *, *, #23788, .F. ) ;
#13183=LINE ( 'NONE', #17088, #21958 ) ;
#13187=ADVANCED_FACE ( 'NONE', ( #22461 ), #12670, .F. ) ;
#13188=EDGE_CURVE ( 'NONE', #4993, #7176, #2309, .T. ) ;
#13190=DIRECTION ( 'NONE',  ( -0.000000000000000000, -0.000000000000000000, 1.000000000000000000 ) ) ;
#13198=LINE ( 'NONE', #1760, #1814 ) ;
#13205=DIRECTION ( 'NONE',  ( -0.000000000000000000, -0.000000000000000000, -1.000000000000000000 ) ) ;
#13208=AXIS2_PLACEMENT_3D ( 'NONE', #12005, #10167, #8355 ) ;
#13213=EDGE_CURVE ( 'NONE', #10867, #1818, #2060, .T. ) ;
#13214=DIRECTION ( 'NONE',  ( 0.000000000000000000, 0.000000000000000000, 1.000000000000000000 ) ) ;
#13237=AXIS2_PLACEMENT_3D ( 'NONE', #5486, #6967, #20151 ) ;
#13243=DIRECTION ( 'NONE',  ( -0.7089874389501510388, 0.7052211081716897034, 0.000000000000000000 ) ) ;
#13246=EDGE_CURVE ( 'NONE', #19429, #4705, #6065, .T. ) ;
#13251=( LENGTH_UNIT ( ) NAMED_UNIT ( * ) SI_UNIT ( .MILLI., .METRE. ) );
#13252=AXIS2_PLACEMENT_3D ( 'NONE', #22369, #5769, #22493 ) ;
#13263=EDGE_CURVE ( 'NONE', #7176, #10867, #11567, .T. ) ;
#13273=CARTESIAN_POINT ( 'NONE',  ( -1.999999999999996669, 45.00000000000000000, -8.673617379884035472E-16 ) ) ;
#13283=FACE_OUTER_BOUND ( 'NONE', #9014, .T. ) ;
#13284=AXIS2_PLACEMENT_3D ( 'NONE', #14738, #12424, #3284 ) ;
#13291=VERTEX_POINT ( 'NONE', #20207 ) ;
#13301=CARTESIAN_POINT ( 'NONE',  ( -28.73477696352899002, 42.73830357953206516, 0.000000000000000000 ) ) ;
#13303=FACE_OUTER_BOUND ( 'NONE', #16594, .T. ) ;
#13312=VERTEX_POINT ( 'NONE', #7262 ) ;
#13318=ORIENTED_EDGE ( 'NONE', *, *, #13159, .T. ) ;
#13324=CYLINDRICAL_SURFACE ( 'NONE', #18648, 8.999999999999994671 ) ;
#13326=VERTEX_POINT ( 'NONE', #5434 ) ;
#13329=AXIS2_PLACEMENT_3D ( 'NONE', #9524, #9173, #16975 ) ;
#13331=CARTESIAN_POINT ( 'NONE',  ( 3.890962118697714531E-15, 15.50000000000000000, 7.699999999999998401 ) ) ;
#13355=VECTOR ( 'NONE', #2630, 1000.000000000000000 ) ;
#13370=DIRECTION ( 'NONE',  ( -1.000000000000000000, 0.000000000000000000, 0.000000000000000000 ) ) ;
#13372=CARTESIAN_POINT ( 'NONE',  ( 41.73082370883258818, -27.62204025492844650, -1.500000000000000000 ) ) ;
#13376=AXIS2_PLACEMENT_3D ( 'NONE', #22879, #784, #4584 ) ;
#13383=EDGE_LOOP ( 'NONE', ( #12868, #23360, #10787, #6832 ) ) ;
#13385=VERTEX_POINT ( 'NONE', #3366 ) ;
#13388=CIRCLE ( 'NONE', #5994, 1.499999999999999778 ) ;
#13389=DIRECTION ( 'NONE',  ( -1.000000000000000000, 5.501724186093585079E-16, 0.000000000000000000 ) ) ;
#13412=DIRECTION ( 'NONE',  ( 1.000000000000000000, 0.000000000000000000, 0.000000000000000000 ) ) ;
#13416=DIRECTION ( 'NONE',  ( -1.000000000000000000, 0.000000000000000000, 0.000000000000000000 ) ) ;
#13422=DIRECTION ( 'NONE',  ( -1.000000000000000000, 0.000000000000000000, 0.000000000000000000 ) ) ;
#13426=AXIS2_PLACEMENT_3D ( 'NONE', #22395, #1890, #22746 ) ;
#13428=VERTEX_POINT ( 'NONE', #4325 ) ;
#13430=AXIS2_PLACEMENT_3D ( 'NONE', #2780, #146, #22481 ) ;
#13441=VERTEX_POINT ( 'NONE', #3954 ) ;
#13442=DIRECTION ( 'NONE',  ( -1.000000000000000000, 0.000000000000000000, 0.000000000000000000 ) ) ;
#13449=AXIS2_PLACEMENT_3D ( 'NONE', #5303, #15139, #11340 ) ;
#13452=LINE ( 'NONE', #10131, #20477 ) ;
#13457=EDGE_LOOP ( 'NONE', ( #20569, #21757, #13826, #12654 ) ) ;
#13470=ORIENTED_EDGE ( 'NONE', *, *, #15832, .T. ) ;
#13482=EDGE_CURVE ( 'NONE', #22724, #12105, #2587, .T. ) ;
#13498=CYLINDRICAL_SURFACE ( 'NONE', #235, 4.249999999999996447 ) ;
#13511=ORIENTED_EDGE ( 'NONE', *, *, #139, .T. ) ;
#13523=DIRECTION ( 'NONE',  ( -0.000000000000000000, 0.000000000000000000, -1.000000000000000000 ) ) ;
#13524=CARTESIAN_POINT ( 'NONE',  ( 40.66734255040738333, 26.56420859267091217, -1.500000000000000000 ) ) ;
#13529=LINE ( 'NONE', #20972, #3327 ) ;
#13532=FACE_OUTER_BOUND ( 'NONE', #10306, .T. ) ;
#13535=CARTESIAN_POINT ( 'NONE',  ( 35.99999999999992184, 59.99999999999998579, 0.000000000000000000 ) ) ;
#13545=DIRECTION ( 'NONE',  ( 0.000000000000000000, -4.625929269271485322E-15, -1.000000000000000000 ) ) ;
#13560=DIRECTION ( 'NONE',  ( -1.000000000000000000, 0.000000000000000000, -0.000000000000000000 ) ) ;
#13573=AXIS2_PLACEMENT_3D ( 'NONE', #3859, #15066, #213 ) ;
#13580=VERTEX_POINT ( 'NONE', #8335 ) ;
#13581=ORIENTED_EDGE ( 'NONE', *, *, #23958, .F. ) ;
#13582=ORIENTED_EDGE ( 'NONE', *, *, #4150, .F. ) ;
#13584=ORIENTED_EDGE ( 'NONE', *, *, #1498, .T. ) ;
#13585=CARTESIAN_POINT ( 'NONE',  ( -24.75000000000000000, 29.50000000000000000, 14.00000000000000178 ) ) ;
#13587=DIRECTION ( 'NONE',  ( -0.000000000000000000, -0.000000000000000000, -1.000000000000000000 ) ) ;
#13588=AXIS2_PLACEMENT_3D ( 'NONE', #8425, #866, #17948 ) ;
#13590=DIRECTION ( 'NONE',  ( -1.000000000000000000, 0.000000000000000000, 0.000000000000000000 ) ) ;
#13592=CARTESIAN_POINT ( 'NONE',  ( -36.00000000000001421, 50.99999999999999289, 12.50000000000000000 ) ) ;
#13611=FACE_OUTER_BOUND ( 'NONE', #14812, .T. ) ;
#13612=ADVANCED_FACE ( 'NONE', ( #23253 ), #17378, .F. ) ;
#13616=VERTEX_POINT ( 'NONE', #3693 ) ;
#13618=CARTESIAN_POINT ( 'NONE',  ( -14.99999999999999645, 15.50000000000000178, 19.70000000000000284 ) ) ;
#13620=FACE_OUTER_BOUND ( 'NONE', #14471, .T. ) ;
#13623=VERTEX_POINT ( 'NONE', #9286 ) ;
#13631=CIRCLE ( 'NONE', #5075, 8.000000000000000000 ) ;
#13638=ADVANCED_FACE ( 'NONE', ( #23957 ), #10872, .F. ) ;
#13639=DIRECTION ( 'NONE',  ( -0.000000000000000000, -0.000000000000000000, -1.000000000000000000 ) ) ;
#13646=DIRECTION ( 'NONE',  ( 0.000000000000000000, 0.000000000000000000, 1.000000000000000000 ) ) ;
#13651=VERTEX_POINT ( 'NONE', #12593 ) ;
#13661=DIRECTION ( 'NONE',  ( -1.000000000000000000, 0.000000000000000000, 0.000000000000000000 ) ) ;
#13669=ORIENTED_EDGE ( 'NONE', *, *, #7469, .F. ) ;
#13685=ORIENTED_EDGE ( 'NONE', *, *, #13755, .T. ) ;
#13686=ORIENTED_EDGE ( 'NONE', *, *, #1725, .F. ) ;
#13698=LINE ( 'NONE', #4451, #4797 ) ;
#13700=FACE_OUTER_BOUND ( 'NONE', #3775, .T. ) ;
#13701=DIRECTION ( 'NONE',  ( -0.000000000000000000, -0.000000000000000000, -1.000000000000000000 ) ) ;
#13714=AXIS2_PLACEMENT_3D ( 'NONE', #2325, #22953, #11818 ) ;
#13730=FACE_OUTER_BOUND ( 'NONE', #13383, .T. ) ;
#13736=DIRECTION ( 'NONE',  ( -1.000000000000000000, 0.000000000000000000, 0.000000000000000000 ) ) ;
#13737=AXIS2_PLACEMENT_3D ( 'NONE', #20114, #14595, #3748 ) ;
#13746=ORIENTED_EDGE ( 'NONE', *, *, #15903, .F. ) ;
#13747=AXIS2_PLACEMENT_3D ( 'NONE', #5491, #9262, #16709 ) ;
#13752=ADVANCED_FACE ( 'NONE', ( #13303 ), #16976, .F. ) ;
#13754=UNCERTAINTY_MEASURE_WITH_UNIT (LENGTH_MEASURE( 1.000000000000000082E-05 ), #11770, 'distance_accuracy_value', 'NONE');
#13755=EDGE_CURVE ( 'NONE', #7176, #6097, #19365, .T. ) ;
#13767=DIRECTION ( 'NONE',  ( 0.000000000000000000, 0.000000000000000000, -1.000000000000000000 ) ) ;
#13786=ADVANCED_FACE ( 'NONE', ( #8907 ), #7625, .F. ) ;
#13807=EDGE_CURVE ( 'NONE', #13385, #18344, #10746, .T. ) ;
#13826=ORIENTED_EDGE ( 'NONE', *, *, #13213, .T. ) ;
#13836=DIRECTION ( 'NONE',  ( 1.000000000000000000, 0.000000000000000000, 0.000000000000000000 ) ) ;
#13840=CARTESIAN_POINT ( 'NONE',  ( 29.00000000000000355, -29.50000000000000000, -3.000000000000000000 ) ) ;
#13851=EDGE_CURVE ( 'NONE', #4606, #13385, #14513, .T. ) ;
#13855=EDGE_LOOP ( 'NONE', ( #18751, #903 ) ) ;
#13898=CARTESIAN_POINT ( 'NONE',  ( -40.50000000000000000, -51.00000000000000711, 0.5000000000000004441 ) ) ;
#13900=VECTOR ( 'NONE', #2511, 999.9999999999998863 ) ;
#13908=ORIENTED_EDGE ( 'NONE', *, *, #8215, .F. ) ;
#13918=CARTESIAN_POINT ( 'NONE',  ( 30.68762588338048403, 45.64284848299539732, -3.000000000000000000 ) ) ;
#13928=CYLINDRICAL_SURFACE ( 'NONE', #9096, 1.500000000000002887 ) ;
#13929=DIRECTION ( 'NONE',  ( -0.000000000000000000, -0.000000000000000000, -1.000000000000000000 ) ) ;
#13933=EDGE_CURVE ( 'NONE', #3090, #13127, #8552, .T. ) ;
#13935=DIRECTION ( 'NONE',  ( -1.000000000000000000, 0.000000000000000000, 0.000000000000000000 ) ) ;
#13942=DIRECTION ( 'NONE',  ( 0.000000000000000000, 0.000000000000000000, -1.000000000000000000 ) ) ;
#13946=VERTEX_POINT ( 'NONE', #6863 ) ;
#13947=DIRECTION ( 'NONE',  ( -0.000000000000000000, -0.000000000000000000, 1.000000000000000000 ) ) ;
#13949=EDGE_CURVE ( 'NONE', #6921, #2673, #16604, .T. ) ;
#13954=EDGE_CURVE ( 'NONE', #17382, #6547, #14053, .T. ) ;
#13962=LINE ( 'NONE', #6640, #7960 ) ;
#13973=ORIENTED_EDGE ( 'NONE', *, *, #6689, .F. ) ;
#13974=CARTESIAN_POINT ( 'NONE',  ( 42.00000000000000000, 25.22443390181681622, -3.000000000000000000 ) ) ;
#13978=ORIENTED_EDGE ( 'NONE', *, *, #10942, .F. ) ;
#14000=ORIENTED_EDGE ( 'NONE', *, *, #23057, .F. ) ;
#14006=PLANE ( 'NONE',  #16579 ) ;
#14013=CYLINDRICAL_SURFACE ( 'NONE', #7838, 1.500000000000000000 ) ;
#14022=ORIENTED_EDGE ( 'NONE', *, *, #14449, .T. ) ;
#14037=ORIENTED_EDGE ( 'NONE', *, *, #2291, .F. ) ;
#14038=CARTESIAN_POINT ( 'NONE',  ( 41.73082370883257397, -27.62204025492843940, -1.500000000000000000 ) ) ;
#14045=CARTESIAN_POINT ( 'NONE',  ( -36.00000000000001421, 50.99999999999999289, 0.5000000000000004441 ) ) ;
#14046=ORIENTED_EDGE ( 'NONE', *, *, #8035, .T. ) ;
#14047=DIRECTION ( 'NONE',  ( 0.000000000000000000, 0.000000000000000000, 1.000000000000000000 ) ) ;
#14048=VERTEX_POINT ( 'NONE', #17319 ) ;
#14052=CARTESIAN_POINT ( 'NONE',  ( -41.99999999999997158, -25.22443390181683043, -1.500000000000000000 ) ) ;
#14053=LINE ( 'NONE', #21751, #23255 ) ;
#14057=EDGE_CURVE ( 'NONE', #21225, #3090, #17400, .T. ) ;
#14059=LINE ( 'NONE', #21507, #6865 ) ;
#14065=DIRECTION ( 'NONE',  ( 1.000000000000000000, 0.000000000000000000, 0.000000000000000000 ) ) ;
#14071=DIRECTION ( 'NONE',  ( -1.000000000000000000, 0.000000000000000000, 0.000000000000000000 ) ) ;
#14080=ADVANCED_FACE ( 'NONE', ( #4279 ), #5334, .F. ) ;
#14082=ORIENTED_EDGE ( 'NONE', *, *, #11736, .T. ) ;
#14084=EDGE_CURVE ( 'NONE', #13109, #14877, #11546, .T. ) ;
#14089=AXIS2_PLACEMENT_3D ( 'NONE', #7219, #10967, #18447 ) ;
#14095=DIRECTION ( 'NONE',  ( -0.000000000000000000, -0.000000000000000000, 1.000000000000000000 ) ) ;
#14103=EDGE_CURVE ( 'NONE', #10649, #12142, #1225, .T. ) ;
#14106=CARTESIAN_POINT ( 'NONE',  ( -35.99999999999994316, -60.00000000000000000, 12.50000000000000000 ) ) ;
#14116=EDGE_CURVE ( 'NONE', #17727, #910, #7641, .T. ) ;
#14121=VECTOR ( 'NONE', #8756, 1000.000000000000000 ) ;
#14128=DIRECTION ( 'NONE',  ( -1.000000000000000000, 0.000000000000000000, 0.000000000000000000 ) ) ;
#14140=CIRCLE ( 'NONE', #22341, 2.024999999999999911 ) ;
#14141=EDGE_CURVE ( 'NONE', #13651, #23135, #18971, .T. ) ;
#14142=AXIS2_PLACEMENT_3D ( 'NONE', #23074, #15237, #19061 ) ;
#14143=ORIENTED_EDGE ( 'NONE', *, *, #15418, .F. ) ;
#14147=DIRECTION ( 'NONE',  ( -0.000000000000000000, -0.000000000000000000, -1.000000000000000000 ) ) ;
#14172=DIRECTION ( 'NONE',  ( -0.000000000000000000, -0.000000000000000000, 1.000000000000000000 ) ) ;
#14173=ORIENTED_EDGE ( 'NONE', *, *, #17926, .T. ) ;
#14180=ORIENTED_EDGE ( 'NONE', *, *, #23368, .F. ) ;
#14184=DIRECTION ( 'NONE',  ( 0.000000000000000000, 0.000000000000000000, -1.000000000000000000 ) ) ;
#14189=CARTESIAN_POINT ( 'NONE',  ( 1.999999999999996669, 45.00000000000000000, -8.673617379884035472E-16 ) ) ;
#14192=AXIS2_PLACEMENT_3D ( 'NONE', #15072, #13243, #22651 ) ;
#14198=CARTESIAN_POINT ( 'NONE',  ( 40.66734255040735491, -26.56420859267090862, -3.000000000000000000 ) ) ;
#14201=ORIENTED_EDGE ( 'NONE', *, *, #1253, .F. ) ;
#14219=EDGE_CURVE ( 'NONE', #9321, #12610, #7275, .T. ) ;
#14233=AXIS2_PLACEMENT_3D ( 'NONE', #9397, #7701, #1634 ) ;
#14248=DIRECTION ( 'NONE',  ( -0.000000000000000000, -0.000000000000000000, 1.000000000000000000 ) ) ;
#14254=EDGE_LOOP ( 'NONE', ( #4442, #18528 ) ) ;
#14273=ORIENTED_EDGE ( 'NONE', *, *, #16991, .T. ) ;
#14282=DIRECTION ( 'NONE',  ( -0.000000000000000000, -0.000000000000000000, -1.000000000000000000 ) ) ;
#14283=ORIENTED_EDGE ( 'NONE', *, *, #7755, .T. ) ;
#14297=ORIENTED_EDGE ( 'NONE', *, *, #1801, .F. ) ;
#14299=EDGE_CURVE ( 'NONE', #10832, #2783, #3009, .T. ) ;
#14300=DIRECTION ( 'NONE',  ( -1.000000000000000000, 0.000000000000000000, 0.000000000000000000 ) ) ;
#14301=CARTESIAN_POINT ( 'NONE',  ( 27.99999999999998934, 50.99999999999999289, 0.5000000000000000000 ) ) ;
#14304=ADVANCED_FACE ( 'NONE', ( #18185 ), #17750, .F. ) ;
#14309=DIRECTION ( 'NONE',  ( -1.000000000000000000, 0.000000000000000000, 0.000000000000000000 ) ) ;
#14317=ADVANCED_FACE ( 'NONE', ( #10713 ), #20090, .F. ) ;
#14323=EDGE_LOOP ( 'NONE', ( #4073, #12857 ) ) ;
#14333=AXIS2_PLACEMENT_3D ( 'NONE', #18352, #15037, #24083 ) ;
#14351=EDGE_CURVE ( 'NONE', #16608, #17944, #5282, .T. ) ;
#14358=ORIENTED_EDGE ( 'NONE', *, *, #8919, .T. ) ;
#14364=CARTESIAN_POINT ( 'NONE',  ( 28.99999999999998579, -29.49999999999999645, -3.000000000000000000 ) ) ;
#14376=DIRECTION ( 'NONE',  ( -1.000000000000000000, 0.000000000000000000, 0.000000000000000000 ) ) ;
#14381=LINE ( 'NONE', #6480, #16466 ) ;
#14382=EDGE_CURVE ( 'NONE', #19008, #4863, #22045, .T. ) ;
#14383=EDGE_CURVE ( 'NONE', #2260, #6140, #813, .T. ) ;
#14385=CONICAL_SURFACE ( 'NONE', #13208, 4.249999999999996447, 1.029744258676654090 ) ;
#14389=CARTESIAN_POINT ( 'NONE',  ( 35.99999999999999289, 50.99999999999999289, 0.000000000000000000 ) ) ;
#14390=CARTESIAN_POINT ( 'NONE',  ( 43.50000000000002132, 50.99999999999998579, 0.000000000000000000 ) ) ;
#14403=DIRECTION ( 'NONE',  ( -0.7071067811865474617, 0.000000000000000000, -0.7071067811865474617 ) ) ;
#14404=EDGE_CURVE ( 'NONE', #12988, #1921, #4852, .T. ) ;
#14407=EDGE_LOOP ( 'NONE', ( #11624, #18464, #20294, #23122 ) ) ;
#14423=ORIENTED_EDGE ( 'NONE', *, *, #5570, .T. ) ;
#14424=VERTEX_POINT ( 'NONE', #12128 ) ;
#14425=ORIENTED_EDGE ( 'NONE', *, *, #14103, .F. ) ;
#14429=CARTESIAN_POINT ( 'NONE',  ( -39.99999999999999289, 15.50000000000000000, 12.50000000000000000 ) ) ;
#14432=ORIENTED_EDGE ( 'NONE', *, *, #4552, .T. ) ;
#14449=EDGE_CURVE ( 'NONE', #10996, #20777, #22263, .T. ) ;
#14453=EDGE_LOOP ( 'NONE', ( #12497, #7624, #15650 ) ) ;
#14454=EDGE_CURVE ( 'NONE', #3651, #15771, #3343, .T. ) ;
#14460=FACE_OUTER_BOUND ( 'NONE', #14529, .T. ) ;
#14465=LINE ( 'NONE', #8974, #5934 ) ;
#14467=DIRECTION ( 'NONE',  ( -0.000000000000000000, -0.000000000000000000, -1.000000000000000000 ) ) ;
#14470=DIRECTION ( 'NONE',  ( -0.000000000000000000, -0.000000000000000000, -1.000000000000000000 ) ) ;
#14471=EDGE_LOOP ( 'NONE', ( #10163, #20785, #6873, #14757 ) ) ;
#14481=ADVANCED_FACE ( 'NONE', ( #23748 ), #5540, .F. ) ;
#14483=CARTESIAN_POINT ( 'NONE',  ( 40.66734255040736201, -26.56420859267091217, -1.500000000000000000 ) ) ;
#14486=DIRECTION ( 'NONE',  ( -0.000000000000000000, -0.000000000000000000, -1.000000000000000000 ) ) ;
#14490=DIRECTION ( 'NONE',  ( -1.000000000000000000, 0.000000000000000000, 0.000000000000000000 ) ) ;
#14495=AXIS2_PLACEMENT_3D ( 'NONE', #16369, #8823, #14309 ) ;
#14500=FACE_OUTER_BOUND ( 'NONE', #18144, .T. ) ;
#14504=CARTESIAN_POINT ( 'NONE',  ( 40.66734255040738333, 26.56420859267091217, -1.500000000000000000 ) ) ;
#14513=LINE ( 'NONE', #3433, #256 ) ;
#14527=FACE_OUTER_BOUND ( 'NONE', #3045, .T. ) ;
#14529=EDGE_LOOP ( 'NONE', ( #696, #22355 ) ) ;
#14533=AXIS2_PLACEMENT_3D ( 'NONE', #13372, #20340, #5815 ) ;
#14535=DIRECTION ( 'NONE',  ( -1.000000000000000000, 0.000000000000000000, 0.000000000000000000 ) ) ;
#14537=ADVANCED_FACE ( 'NONE', ( #20427 ), #3719, .T. ) ;
#14574=ADVANCED_FACE ( 'NONE', ( #6058 ), #13498, .F. ) ;
#14576=ORIENTED_EDGE ( 'NONE', *, *, #7494, .F. ) ;
#14582=ORIENTED_EDGE ( 'NONE', *, *, #12970, .F. ) ;
#14583=ORIENTED_EDGE ( 'NONE', *, *, #8739, .T. ) ;
#14591=ADVANCED_FACE ( 'NONE', ( #13611 ), #4350, .F. ) ;
#14592=AXIS2_PLACEMENT_3D ( 'NONE', #16781, #13012, #22908 ) ;
#14593=CARTESIAN_POINT ( 'NONE',  ( -41.73082370883260239, 29.50000000000000711, 0.000000000000000000 ) ) ;
#14595=DIRECTION ( 'NONE',  ( 0.000000000000000000, 0.000000000000000000, -1.000000000000000000 ) ) ;
#14598=ORIENTED_EDGE ( 'NONE', *, *, #20637, .T. ) ;
#14604=LINE ( 'NONE', #19873, #7930 ) ;
#14606=DIRECTION ( 'NONE',  ( 1.000000000000000000, 0.000000000000000000, 0.000000000000000000 ) ) ;
#14616=VECTOR ( 'NONE', #17584, 1000.000000000000000 ) ;
#14619=CARTESIAN_POINT ( 'NONE',  ( 0.000000000000000000, -45.00000000000000000, -8.673617379884035472E-16 ) ) ;
#14620=CARTESIAN_POINT ( 'NONE',  ( 41.73082370883257397, -27.62204025492843940, -3.000000000000000000 ) ) ;
#14623=AXIS2_PLACEMENT_3D ( 'NONE', #23213, #11958, #13935 ) ;
#14654=DIRECTION ( 'NONE',  ( -0.000000000000000000, -0.000000000000000000, -1.000000000000000000 ) ) ;
#14656=AXIS2_PLACEMENT_3D ( 'NONE', #19909, #5035, #1843 ) ;
#14662=ADVANCED_FACE ( 'NONE', ( #4845 ), #1425, .F. ) ;
#14667=LINE ( 'NONE', #16725, #7883 ) ;
#14668=CIRCLE ( 'NONE', #4168, 5.000000000000000888 ) ;
#14683=ORIENTED_EDGE ( 'NONE', *, *, #1516, .T. ) ;
#14685=FACE_BOUND ( 'NONE', #20848, .T. ) ;
#14703=EDGE_LOOP ( 'NONE', ( #1114, #17942, #15356, #1157, #8418, #228, #10703, #22747, #773, #12483, #5785, #7147, #13584, #14583, #22054, #12022, #16358, #10678, #11433, #12006, #381, #4704, #17491, #3715 ) ) ;
#14711=DIRECTION ( 'NONE',  ( -0.000000000000000000, -0.000000000000000000, 1.000000000000000000 ) ) ;
#14714=CARTESIAN_POINT ( 'NONE',  ( 0.000000000000000000, 45.00000000000000000, -8.673617379884035472E-16 ) ) ;
#14715=CARTESIAN_POINT ( 'NONE',  ( 35.99999999999999289, -51.00000000000000711, 0.5000000000000000000 ) ) ;
#14723=ORIENTED_EDGE ( 'NONE', *, *, #13755, .F. ) ;
#14738=CARTESIAN_POINT ( 'NONE',  ( 35.99999999999999289, 50.99999999999999289, 12.50000000000000000 ) ) ;
#14740=DIRECTION ( 'NONE',  ( 1.000000000000000000, -0.000000000000000000, 0.000000000000000000 ) ) ;
#14747=ORIENTED_EDGE ( 'NONE', *, *, #3941, .F. ) ;
#14748=CARTESIAN_POINT ( 'NONE',  ( -33.24999999999999289, 29.50000000000000000, 14.00000000000000178 ) ) ;
#14757=ORIENTED_EDGE ( 'NONE', *, *, #22099, .F. ) ;
#14766=CARTESIAN_POINT ( 'NONE',  ( 3.890962118697714531E-15, 15.50000000000000000, 19.70000000000000284 ) ) ;
#14767=ADVANCED_FACE ( 'NONE', ( #16644 ), #20502, .F. ) ;
#14789=EDGE_LOOP ( 'NONE', ( #18174, #12584 ) ) ;
#14790=AXIS2_PLACEMENT_3D ( 'NONE', #21200, #20962, #2899 ) ;
#14792=ORIENTED_EDGE ( 'NONE', *, *, #9705, .T. ) ;
#14793=DIRECTION ( 'NONE',  ( 0.000000000000000000, 1.000000000000000000, 0.000000000000000000 ) ) ;
#14794=CARTESIAN_POINT ( 'NONE',  ( -36.00000000000001421, 50.99999999999999289, 12.50000000000000000 ) ) ;
#14795=EDGE_LOOP ( 'NONE', ( #7787, #14082, #7396, #3581 ) ) ;
#14797=ORIENTED_EDGE ( 'NONE', *, *, #20724, .F. ) ;
#14802=CARTESIAN_POINT ( 'NONE',  ( 35.99999999999999289, 50.99999999999999289, 0.000000000000000000 ) ) ;
#14807=ORIENTED_EDGE ( 'NONE', *, *, #14449, .F. ) ;
#14811=EDGE_CURVE ( 'NONE', #11720, #22066, #633, .T. ) ;
#14812=EDGE_LOOP ( 'NONE', ( #14358, #6033, #6226, #23580 ) ) ;
#14820=DIRECTION ( 'NONE',  ( -0.7052211081716905916, 0.7089874389501501506, 0.000000000000000000 ) ) ;
#14844=ORIENTED_EDGE ( 'NONE', *, *, #13949, .T. ) ;
#14847=DIRECTION ( 'NONE',  ( -1.000000000000000000, 0.000000000000000000, 0.000000000000000000 ) ) ;
#14854=CARTESIAN_POINT ( 'NONE',  ( 28.73477696352899358, -42.73830357953205805, 0.000000000000000000 ) ) ;
#14855=AXIS2_PLACEMENT_3D ( 'NONE', #12619, #10890, #3716 ) ;
#14863=VERTEX_POINT ( 'NONE', #19658 ) ;
#14865=ADVANCED_FACE ( 'NONE', ( #2932 ), #10360, .F. ) ;
#14876=VERTEX_POINT ( 'NONE', #1698 ) ;
#14877=VERTEX_POINT ( 'NONE', #12898 ) ;
#14878=CARTESIAN_POINT ( 'NONE',  ( -41.99999999999997158, -25.22443390181683043, -1.500000000000000000 ) ) ;
#14880=EDGE_CURVE ( 'NONE', #22249, #23011, #19346, .T. ) ;
#14881=ORIENTED_EDGE ( 'NONE', *, *, #8215, .T. ) ;
#14885=AXIS2_PLACEMENT_3D ( 'NONE', #9890, #7807, #168 ) ;
#14895=LINE ( 'NONE', #3691, #12473 ) ;
#14898=DIRECTION ( 'NONE',  ( 0.7052211081716905916, 0.7089874389501501506, 0.000000000000000000 ) ) ;
#14907=AXIS2_PLACEMENT_3D ( 'NONE', #3002, #12251, #6900 ) ;
#14912=CIRCLE ( 'NONE', #2868, 49.99999999999998579 ) ;
#14917=LINE ( 'NONE', #13099, #1713 ) ;
#14918=DIRECTION ( 'NONE',  ( -1.000000000000000000, 0.000000000000000000, 0.000000000000000000 ) ) ;
#14920=DIRECTION ( 'NONE',  ( -1.000000000000000000, 0.000000000000000000, 0.000000000000000000 ) ) ;
#14934=CARTESIAN_POINT ( 'NONE',  ( 41.99999999999997158, -25.22443390181681622, -3.000000000000000000 ) ) ;
#14937=ORIENTED_EDGE ( 'NONE', *, *, #16385, .F. ) ;
#14972=CIRCLE ( 'NONE', #11859, 1.500000000000000222 ) ;
#14980=ADVANCED_FACE ( 'NONE', ( #6682 ), #3133, .F. ) ;
#15005=ORIENTED_EDGE ( 'NONE', *, *, #17422, .F. ) ;
#15008=AXIS2_PLACEMENT_3D ( 'NONE', #19580, #1273, #10288 ) ;
#15019=DIRECTION ( 'NONE',  ( -1.000000000000000000, 0.000000000000000000, 0.000000000000000000 ) ) ;
#15022=ORIENTED_EDGE ( 'NONE', *, *, #5572, .T. ) ;
#15037=DIRECTION ( 'NONE',  ( 0.000000000000000000, 0.000000000000000000, 1.000000000000000000 ) ) ;
#15039=DIRECTION ( 'NONE',  ( -0.000000000000000000, 1.000000000000000000, -0.000000000000000000 ) ) ;
#15040=CARTESIAN_POINT ( 'NONE',  ( 27.89784171216406961, 41.49349862090490859, -3.000000000000000000 ) ) ;
#15052=VECTOR ( 'NONE', #13190, 1000.000000000000000 ) ;
#15063=CARTESIAN_POINT ( 'NONE',  ( -40.66734255040736201, -26.56420859267092283, -3.000000000000000000 ) ) ;
#15066=DIRECTION ( 'NONE',  ( 0.000000000000000000, 0.000000000000000000, -1.000000000000000000 ) ) ;
#15071=CARTESIAN_POINT ( 'NONE',  ( 15.00000000000000355, 15.50000000000000000, 14.70000000000000284 ) ) ;
#15072=CARTESIAN_POINT ( 'NONE',  ( 40.66734255040736201, -26.56420859267091217, -3.000000000000000000 ) ) ;
#15076=EDGE_LOOP ( 'NONE', ( #14297, #1676 ) ) ;
#15078=ORIENTED_EDGE ( 'NONE', *, *, #15339, .T. ) ;
#15089=DIRECTION ( 'NONE',  ( -1.000000000000000000, 0.000000000000000000, 0.000000000000000000 ) ) ;
#15101=AXIS2_PLACEMENT_3D ( 'NONE', #12578, #6877, #16489 ) ;
#15122=VECTOR ( 'NONE', #7684, 1000.000000000000000 ) ;
#15124=CARTESIAN_POINT ( 'NONE',  ( 0.000000000000000000, 0.000000000000000000, -1.500000000000000000 ) ) ;
#15130=DIRECTION ( 'NONE',  ( -0.000000000000000000, -0.000000000000000000, -1.000000000000000000 ) ) ;
#15131=DIRECTION ( 'NONE',  ( 0.7071067811865292541, 8.659560562354708526E-17, -0.7071067811865658914 ) ) ;
#15132=FACE_OUTER_BOUND ( 'NONE', #14407, .T. ) ;
#15134=EDGE_CURVE ( 'NONE', #47, #20318, #20858, .T. ) ;
#15139=DIRECTION ( 'NONE',  ( 0.000000000000000000, 0.000000000000000000, 1.000000000000000000 ) ) ;
#15143=DIRECTION ( 'NONE',  ( -1.000000000000000000, 0.000000000000000000, 0.000000000000000000 ) ) ;
#15149=CARTESIAN_POINT ( 'NONE',  ( 3.890962118697714531E-15, 15.50000000000000000, 19.20000000000000995 ) ) ;
#15158=VECTOR ( 'NONE', #14095, 1000.000000000000000 ) ;
#15159=EDGE_CURVE ( 'NONE', #15532, #20601, #14972, .T. ) ;
#15162=ORIENTED_EDGE ( 'NONE', *, *, #8919, .F. ) ;
#15167=DIRECTION ( 'NONE',  ( -1.000000000000000000, 0.000000000000000000, 0.000000000000000000 ) ) ;
#15184=CARTESIAN_POINT ( 'NONE',  ( -1.999999999999997113, -45.00000000000000000, -2.974999999999996092 ) ) ;
#15185=ORIENTED_EDGE ( 'NONE', *, *, #1233, .T. ) ;
#15196=DIRECTION ( 'NONE',  ( 0.000000000000000000, 0.000000000000000000, -1.000000000000000000 ) ) ;
#15202=DIRECTION ( 'NONE',  ( -0.000000000000000000, -0.000000000000000000, 1.000000000000000000 ) ) ;
#15209=CONICAL_SURFACE ( 'NONE', #22262, 5.025000000000002132, 0.7853981633974482790 ) ;
#15211=VERTEX_POINT ( 'NONE', #18262 ) ;
#15219=AXIS2_PLACEMENT_3D ( 'NONE', #22209, #21964, #10723 ) ;
#15222=CIRCLE ( 'NONE', #14089, 1.499999999999994449 ) ;
#15224=EDGE_CURVE ( 'NONE', #10152, #19491, #23991, .T. ) ;
#15232=EDGE_CURVE ( 'NONE', #3029, #5970, #12756, .T. ) ;
#15237=DIRECTION ( 'NONE',  ( -0.000000000000000000, -0.000000000000000000, -1.000000000000000000 ) ) ;
#15241=ORIENTED_EDGE ( 'NONE', *, *, #1801, .T. ) ;
#15247=DIRECTION ( 'NONE',  ( -0.000000000000000000, -0.000000000000000000, -1.000000000000000000 ) ) ;
#15248=ORIENTED_EDGE ( 'NONE', *, *, #606, .T. ) ;
#15260=AXIS2_PLACEMENT_3D ( 'NONE', #8533, #2689, #6841 ) ;
#15273=CARTESIAN_POINT ( 'NONE',  ( -30.68762588338048403, 45.64284848299540442, 0.000000000000000000 ) ) ;
#15275=ORIENTED_EDGE ( 'NONE', *, *, #8736, .F. ) ;
#15285=EDGE_LOOP ( 'NONE', ( #6821, #17988, #9778 ) ) ;
#15287=FACE_OUTER_BOUND ( 'NONE', #23064, .T. ) ;
#15297=DIRECTION ( 'NONE',  ( -0.000000000000000000, -0.000000000000000000, -1.000000000000000000 ) ) ;
#15303=AXIS2_PLACEMENT_3D ( 'NONE', #6696, #3271, #14128 ) ;
#15307=FACE_OUTER_BOUND ( 'NONE', #1957, .T. ) ;
#15321=( NAMED_UNIT ( * ) SI_UNIT ( $, .STERADIAN. ) SOLID_ANGLE_UNIT ( ) );
#15337=CARTESIAN_POINT ( 'NONE',  ( 30.32370777929699202, 42.16181938034194587, 0.000000000000000000 ) ) ;
#15339=EDGE_CURVE ( 'NONE', #14877, #19090, #6163, .T. ) ;
#15356=ORIENTED_EDGE ( 'NONE', *, *, #20506, .T. ) ;
#15374=FACE_OUTER_BOUND ( 'NONE', #17269, .T. ) ;
#15384=CARTESIAN_POINT ( 'NONE',  ( 27.89784171216407316, -41.49349862090490149, -3.000000000000000000 ) ) ;
#15390=ADVANCED_FACE ( 'NONE', ( #15287 ), #1687, .F. ) ;
#15394=AXIS2_PLACEMENT_3D ( 'NONE', #5319, #10892, #18359 ) ;
#15395=VECTOR ( 'NONE', #9141, 1000.000000000000000 ) ;
#15400=DIRECTION ( 'NONE',  ( -0.000000000000000000, -0.000000000000000000, 1.000000000000000000 ) ) ;
#15404=CIRCLE ( 'NONE', #1074, 15.00000000000000000 ) ;
#15412=CYLINDRICAL_SURFACE ( 'NONE', #21974, 4.249999999999996447 ) ;
#15414=AXIS2_PLACEMENT_3D ( 'NONE', #14620, #22090, #7298 ) ;
#15416=EDGE_LOOP ( 'NONE', ( #10877, #12289, #19281 ) ) ;
#15418=EDGE_CURVE ( 'NONE', #13651, #15766, #11629, .T. ) ;
#15420=ORIENTED_EDGE ( 'NONE', *, *, #19691, .T. ) ;
#15421=EDGE_CURVE ( 'NONE', #5924, #6139, #16080, .T. ) ;
#15422=ORIENTED_EDGE ( 'NONE', *, *, #23743, .T. ) ;
#15425=DIRECTION ( 'NONE',  ( 0.000000000000000000, -1.000000000000000000, 0.000000000000000000 ) ) ;
#15436=ORIENTED_EDGE ( 'NONE', *, *, #3289, .F. ) ;
#15447=CARTESIAN_POINT ( 'NONE',  ( 40.66734255040735491, -26.56420859267090862, -3.000000000000000000 ) ) ;
#15455=ORIENTED_EDGE ( 'NONE', *, *, #5572, .F. ) ;
#15460=CARTESIAN_POINT ( 'NONE',  ( 42.00000000000000000, 25.22443390181681622, -3.000000000000000000 ) ) ;
#15467=EDGE_LOOP ( 'NONE', ( #17879, #12781, #21951, #11344 ) ) ;
#15469=CYLINDRICAL_SURFACE ( 'NONE', #2030, 1.499999999999994449 ) ;
#15472=ORIENTED_EDGE ( 'NONE', *, *, #5774, .T. ) ;
#15480=DIRECTION ( 'NONE',  ( 1.000000000000000000, 0.000000000000000000, 0.000000000000000000 ) ) ;
#15485=CARTESIAN_POINT ( 'NONE',  ( -27.89784171216405895, 41.49349862090491570, -1.500000000000000000 ) ) ;
#15500=CARTESIAN_POINT ( 'NONE',  ( -28.99999999999998579, -29.50000000000000711, -1.500000000000000000 ) ) ;
#15502=EDGE_CURVE ( 'NONE', #9321, #16665, #21168, .T. ) ;
#15516=CARTESIAN_POINT ( 'NONE',  ( -28.00000000000001066, 50.99999999999999289, 0.5000000000000000000 ) ) ;
#15518=VERTEX_POINT ( 'NONE', #11883 ) ;
#15521=CIRCLE ( 'NONE', #13588, 1.499999999999994449 ) ;
#15522=CARTESIAN_POINT ( 'NONE',  ( 40.49999999999998579, -51.00000000000000711, 12.50000000000000000 ) ) ;
#15526=DIRECTION ( 'NONE',  ( -0.000000000000000000, -0.000000000000000000, -1.000000000000000000 ) ) ;
#15527=EDGE_CURVE ( 'NONE', #2131, #10832, #8914, .T. ) ;
#15528=ORIENTED_EDGE ( 'NONE', *, *, #14084, .F. ) ;
#15532=VERTEX_POINT ( 'NONE', #2743 ) ;
#15533=EDGE_LOOP ( 'NONE', ( #21295, #3179 ) ) ;
#15541=DIRECTION ( 'NONE',  ( -1.000000000000000000, 0.000000000000000000, 0.000000000000000000 ) ) ;
#15553=AXIS2_PLACEMENT_3D ( 'NONE', #19480, #6290, #10056 ) ;
#15558=VERTEX_POINT ( 'NONE', #23938 ) ;
#15569=AXIS2_PLACEMENT_3D ( 'NONE', #10113, #8294, #6492 ) ;
#15576=EDGE_CURVE ( 'NONE', #20318, #13109, #20522, .T. ) ;
#15583=ADVANCED_FACE ( 'NONE', ( #5754 ), #18814, .F. ) ;
#15586=ORIENTED_EDGE ( 'NONE', *, *, #3298, .T. ) ;
#15593=ORIENTED_EDGE ( 'NONE', *, *, #6908, .T. ) ;
#15595=DIRECTION ( 'NONE',  ( -0.000000000000000000, -0.000000000000000000, 1.000000000000000000 ) ) ;
#15601=ORIENTED_EDGE ( 'NONE', *, *, #16023, .F. ) ;
#15602=DIRECTION ( 'NONE',  ( 1.000000000000000000, 0.000000000000000000, 0.000000000000000000 ) ) ;
#15603=DIRECTION ( 'NONE',  ( -0.000000000000000000, -0.000000000000000000, -1.000000000000000000 ) ) ;
#15606=VERTEX_POINT ( 'NONE', #20626 ) ;
#15610=EDGE_CURVE ( 'NONE', #11505, #1470, #14912, .T. ) ;
#15623=EDGE_CURVE ( 'NONE', #1878, #12712, #16865, .T. ) ;
#15631=DIRECTION ( 'NONE',  ( -1.000000000000000000, 0.000000000000000000, 0.000000000000000000 ) ) ;
#15635=EDGE_LOOP ( 'NONE', ( #4716, #20671, #23645, #9395 ) ) ;
#15639=VECTOR ( 'NONE', #1989, 1000.000000000000000 ) ;
#15643=DIRECTION ( 'NONE',  ( -0.000000000000000000, -0.000000000000000000, -1.000000000000000000 ) ) ;
#15649=VERTEX_POINT ( 'NONE', #2570 ) ;
#15650=ORIENTED_EDGE ( 'NONE', *, *, #18210, .T. ) ;
#15653=VERTEX_POINT ( 'NONE', #10102 ) ;
#15671=DIRECTION ( 'NONE',  ( -1.000000000000000000, 0.000000000000000000, 0.000000000000000000 ) ) ;
#15676=CIRCLE ( 'NONE', #5548, 15.00000000000000000 ) ;
#15677=DIRECTION ( 'NONE',  ( -0.000000000000000000, -0.000000000000000000, 1.000000000000000000 ) ) ;
#15691=CARTESIAN_POINT ( 'NONE',  ( 30.68762588338046982, -45.64284848299539732, -1.500000000000000000 ) ) ;
#15702=VECTOR ( 'NONE', #12650, 1000.000000000000000 ) ;
#15712=CARTESIAN_POINT ( 'NONE',  ( -28.99999999999999645, 29.50000000000000711, -3.000000000000000000 ) ) ;
#15717=ORIENTED_EDGE ( 'NONE', *, *, #7469, .T. ) ;
#15718=VECTOR ( 'NONE', #15603, 1000.000000000000000 ) ;
#15721=CIRCLE ( 'NONE', #6380, 8.000000000000000000 ) ;
#15722=ORIENTED_EDGE ( 'NONE', *, *, #1019, .T. ) ;
#15723=DIRECTION ( 'NONE',  ( -0.000000000000000000, -0.000000000000000000, -1.000000000000000000 ) ) ;
#15726=VECTOR ( 'NONE', #10891, 1000.000000000000000 ) ;
#15729=CYLINDRICAL_SURFACE ( 'NONE', #7991, 4.499999999999997335 ) ;
#15730=EDGE_CURVE ( 'NONE', #5799, #6174, #19158, .T. ) ;
#15737=CARTESIAN_POINT ( 'NONE',  ( 41.73082370883260239, 27.62204025492843940, -3.000000000000000000 ) ) ;
#15742=DIRECTION ( 'NONE',  ( 1.000000000000000000, 0.000000000000000000, 0.000000000000000000 ) ) ;
#15749=VECTOR ( 'NONE', #10658, 1000.000000000000000 ) ;
#15754=LINE ( 'NONE', #19172, #11829 ) ;
#15766=VERTEX_POINT ( 'NONE', #19662 ) ;
#15771=VERTEX_POINT ( 'NONE', #4901 ) ;
#15777=CARTESIAN_POINT ( 'NONE',  ( 23.97500000000000497, 29.50000000000000000, -3.000000000000000000 ) ) ;
#15782=LINE ( 'NONE', #15522, #8766 ) ;
#15785=CYLINDRICAL_SURFACE ( 'NONE', #20026, 8.000000000000000000 ) ;
#15794=VECTOR ( 'NONE', #5487, 1000.000000000000000 ) ;
#15799=LINE ( 'NONE', #13974, #20905 ) ;
#15807=AXIS2_PLACEMENT_3D ( 'NONE', #2175, #22448, #15089 ) ;
#15808=FACE_OUTER_BOUND ( 'NONE', #21086, .T. ) ;
#15820=DIRECTION ( 'NONE',  ( -0.000000000000000000, -0.000000000000000000, -1.000000000000000000 ) ) ;
#15826=EDGE_LOOP ( 'NONE', ( #11226, #1361, #1870, #19874 ) ) ;
#15828=( GEOMETRIC_REPRESENTATION_CONTEXT ( 3 ) GLOBAL_UNCERTAINTY_ASSIGNED_CONTEXT ( ( #5947 ) ) GLOBAL_UNIT_ASSIGNED_CONTEXT ( ( #13251, #4503, #15321 ) ) REPRESENTATION_CONTEXT ( 'NONE', 'WORKASPACE' ) );
#15829=EDGE_CURVE ( 'NONE', #21225, #10767, #16441, .T. ) ;
#15832=EDGE_CURVE ( 'NONE', #14424, #4806, #9843, .T. ) ;
#15835=AXIS2_PLACEMENT_3D ( 'NONE', #8057, #22598, #5876 ) ;
#15844=CIRCLE ( 'NONE', #9211, 1.499999999999998002 ) ;
#15845=FACE_OUTER_BOUND ( 'NONE', #6535, .T. ) ;
#15851=ORIENTED_EDGE ( 'NONE', *, *, #12448, .T. ) ;
#15884=EDGE_CURVE ( 'NONE', #5796, #12524, #7910, .T. ) ;
#15886=CARTESIAN_POINT ( 'NONE',  ( 2.024999999999999911, 45.00000000000000000, -3.000000000000000000 ) ) ;
#15889=CARTESIAN_POINT ( 'NONE',  ( -36.00000000000001421, 50.99999999999999289, 0.000000000000000000 ) ) ;
#15900=FACE_OUTER_BOUND ( 'NONE', #16337, .T. ) ;
#15901=ORIENTED_EDGE ( 'NONE', *, *, #7755, .F. ) ;
#15903=EDGE_CURVE ( 'NONE', #4207, #20601, #9086, .T. ) ;
#15908=ORIENTED_EDGE ( 'NONE', *, *, #17545, .T. ) ;
#15916=ORIENTED_EDGE ( 'NONE', *, *, #5953, .F. ) ;
#15940=VERTEX_POINT ( 'NONE', #1826 ) ;
#15959=CARTESIAN_POINT ( 'NONE',  ( 8.616390364324422180, 78.23814058202225397, 0.000000000000000000 ) ) ;
#15965=EDGE_LOOP ( 'NONE', ( #10349, #7417, #15005, #3446 ) ) ;
#15982=ORIENTED_EDGE ( 'NONE', *, *, #17384, .F. ) ;
#15983=LINE ( 'NONE', #3064, #3944 ) ;
#15985=DIRECTION ( 'NONE',  ( -0.000000000000000000, -0.000000000000000000, 1.000000000000000000 ) ) ;
#15988=ORIENTED_EDGE ( 'NONE', *, *, #1019, .F. ) ;
#15997=CARTESIAN_POINT ( 'NONE',  ( 40.66734255040738333, 26.56420859267091217, -3.000000000000000000 ) ) ;
#16015=FACE_OUTER_BOUND ( 'NONE', #3951, .T. ) ;
#16017=VERTEX_POINT ( 'NONE', #17163 ) ;
#16023=EDGE_CURVE ( 'NONE', #1549, #5954, #3248, .T. ) ;
#16025=CARTESIAN_POINT ( 'NONE',  ( 0.000000000000000000, -45.00000000000000000, -2.974999999999996092 ) ) ;
#16029=EDGE_LOOP ( 'NONE', ( #4570, #17908, #5828, #6442 ) ) ;
#16033=CONICAL_SURFACE ( 'NONE', #22278, 5.025000000000002132, 0.7853981633974482790 ) ;
#16036=CIRCLE ( 'NONE', #2398, 1.499999999999994449 ) ;
#16045=CARTESIAN_POINT ( 'NONE',  ( -42.00000000000000000, 25.22443390181683043, -3.000000000000000000 ) ) ;
#16056=ADVANCED_FACE ( 'NONE', ( #4252 ), #8011, .F. ) ;
#16080=CIRCLE ( 'NONE', #7890, 17.25000000000000000 ) ;
#16103=VERTEX_POINT ( 'NONE', #6572 ) ;
#16105=LINE ( 'NONE', #2944, #8607 ) ;
#16115=CARTESIAN_POINT ( 'NONE',  ( -28.73477696352898292, -42.73830357953205805, 0.000000000000000000 ) ) ;
#16121=EDGE_CURVE ( 'NONE', #16017, #16103, #23526, .T. ) ;
#16127=FACE_OUTER_BOUND ( 'NONE', #9418, .T. ) ;
#16128=ORIENTED_EDGE ( 'NONE', *, *, #3129, .F. ) ;
#16135=CARTESIAN_POINT ( 'NONE',  ( -35.99999999999993605, -60.00000000000000000, 12.50000000000000000 ) ) ;
#16149=CIRCLE ( 'NONE', #9891, 8.999999999999994671 ) ;
#16179=DIRECTION ( 'NONE',  ( 1.000000000000000000, 0.000000000000000000, 0.000000000000000000 ) ) ;
#16185=VERTEX_POINT ( 'NONE', #1088 ) ;
#16197=FACE_OUTER_BOUND ( 'NONE', #12724, .T. ) ;
#16226=CARTESIAN_POINT ( 'NONE',  ( -24.75000000000000000, 29.50000000000000000, -3.000000000000000000 ) ) ;
#16227=VECTOR ( 'NONE', #11032, 1000.000000000000000 ) ;
#16290=CARTESIAN_POINT ( 'NONE',  ( -41.73082370883260950, 27.62204025492845716, -1.500000000000000000 ) ) ;
#16303=CYLINDRICAL_SURFACE ( 'NONE', #4517, 1.999999999999996669 ) ;
#16305=LINE ( 'NONE', #3615, #19606 ) ;
#16306=EDGE_CURVE ( 'NONE', #22066, #7111, #22758, .T. ) ;
#16308=EDGE_CURVE ( 'NONE', #6942, #1952, #84, .T. ) ;
#16311=CARTESIAN_POINT ( 'NONE',  ( -30.68762588338046982, -45.64284848299540442, -3.000000000000000000 ) ) ;
#16312=DIRECTION ( 'NONE',  ( 1.000000000000000000, 0.000000000000000000, 0.000000000000000000 ) ) ;
#16325=VERTEX_POINT ( 'NONE', #5336 ) ;
#16327=DIRECTION ( 'NONE',  ( -1.000000000000000000, 0.000000000000000000, 0.000000000000000000 ) ) ;
#16328=DIRECTION ( 'NONE',  ( 0.000000000000000000, 0.000000000000000000, -1.000000000000000000 ) ) ;
#16335=DIRECTION ( 'NONE',  ( -0.000000000000000000, -0.000000000000000000, -1.000000000000000000 ) ) ;
#16337=EDGE_LOOP ( 'NONE', ( #14683, #4486, #11488 ) ) ;
#16348=AXIS2_PLACEMENT_3D ( 'NONE', #17335, #9743, #13560 ) ;
#16350=ORIENTED_EDGE ( 'NONE', *, *, #10545, .T. ) ;
#16353=DIRECTION ( 'NONE',  ( -0.000000000000000000, -0.000000000000000000, 1.000000000000000000 ) ) ;
#16358=ORIENTED_EDGE ( 'NONE', *, *, #2579, .T. ) ;
#16360=CARTESIAN_POINT ( 'NONE',  ( -28.99999999999999645, 29.50000000000000000, -3.000000000000000000 ) ) ;
#16369=CARTESIAN_POINT ( 'NONE',  ( 35.99999999999999289, -51.00000000000000711, 0.5000000000000004441 ) ) ;
#16373=( BOUNDED_CURVE ( )  B_SPLINE_CURVE ( 3, ( #14878, #23037, #6312, #5636 ),
 .UNSPECIFIED., .F., .T. ) 
 B_SPLINE_CURVE_WITH_KNOTS ( ( 4, 4 ),
 ( 0.000000000000000000, 1.570796326794896558 ),
 .UNSPECIFIED. ) 
 CURVE ( )  GEOMETRIC_REPRESENTATION_ITEM ( )  RATIONAL_B_SPLINE_CURVE ( ( 1.000000000000000000, 0.8047378541243649375, 0.8047378541243649375, 1.000000000000000000 ) ) 
 REPRESENTATION_ITEM ( '' )  );
#16375=EDGE_CURVE ( 'NONE', #11227, #6327, #18861, .T. ) ;
#16385=EDGE_CURVE ( 'NONE', #4863, #19008, #4050, .T. ) ;
#16386=EDGE_CURVE ( 'NONE', #13623, #19012, #22768, .T. ) ;
#16387=DIRECTION ( 'NONE',  ( -1.000000000000000000, 0.000000000000000000, 0.000000000000000000 ) ) ;
#16396=CARTESIAN_POINT ( 'NONE',  ( -40.50000000000000000, -51.00000000000000711, 12.50000000000000000 ) ) ;
#16402=ADVANCED_FACE ( 'NONE', ( #5805 ), #2634, .F. ) ;
#16418=ORIENTED_EDGE ( 'NONE', *, *, #16755, .F. ) ;
#16423=CARTESIAN_POINT ( 'NONE',  ( 31.49999999999999289, 50.99999999999999289, 12.50000000000000000 ) ) ;
#16441=LINE ( 'NONE', #3771, #8306 ) ;
#16451=DIRECTION ( 'NONE',  ( 1.000000000000000000, 0.000000000000000000, 0.000000000000000000 ) ) ;
#16453=CYLINDRICAL_SURFACE ( 'NONE', #18031, 1.999999999999996669 ) ;
#16454=DIRECTION ( 'NONE',  ( 1.000000000000000000, 0.000000000000000000, 0.000000000000000000 ) ) ;
#16466=VECTOR ( 'NONE', #19786, 1000.000000000000000 ) ;
#16476=EDGE_CURVE ( 'NONE', #2444, #21069, #6410, .T. ) ;
#16481=DIRECTION ( 'NONE',  ( -1.000000000000000000, 0.000000000000000000, 0.000000000000000000 ) ) ;
#16485=CARTESIAN_POINT ( 'NONE',  ( -40.66734255040738333, 26.56420859267091927, -3.000000000000000000 ) ) ;
#16487=CIRCLE ( 'NONE', #9829, 5.024999999999998579 ) ;
#16489=DIRECTION ( 'NONE',  ( -1.000000000000000000, 1.387778780781444492E-15, 0.000000000000000000 ) ) ;
#16516=ORIENTED_EDGE ( 'NONE', *, *, #22772, .F. ) ;
#16517=CIRCLE ( 'NONE', #12630, 8.000000000000000000 ) ;
#16520=VERTEX_POINT ( 'NONE', #19944 ) ;
#16522=DIRECTION ( 'NONE',  ( -1.000000000000000000, 0.000000000000000000, 0.000000000000000000 ) ) ;
#16533=ORIENTED_EDGE ( 'NONE', *, *, #21075, .T. ) ;
#16555=DIRECTION ( 'NONE',  ( 0.000000000000000000, 0.000000000000000000, -1.000000000000000000 ) ) ;
#16564=ORIENTED_EDGE ( 'NONE', *, *, #16916, .T. ) ;
#16565=VERTEX_POINT ( 'NONE', #5423 ) ;
#16571=DIRECTION ( 'NONE',  ( -1.000000000000000000, 0.000000000000000000, 0.000000000000000000 ) ) ;
#16572=VECTOR ( 'NONE', #986, 1000.000000000000000 ) ;
#16579=AXIS2_PLACEMENT_3D ( 'NONE', #6198, #10195, #19628 ) ;
#16592=ORIENTED_EDGE ( 'NONE', *, *, #11588, .T. ) ;
#16593=DIRECTION ( 'NONE',  ( 0.000000000000000000, -0.000000000000000000, 1.000000000000000000 ) ) ;
#16594=EDGE_LOOP ( 'NONE', ( #9240, #15022, #3728, #393 ) ) ;
#16599=DIRECTION ( 'NONE',  ( -0.000000000000000000, -0.000000000000000000, -1.000000000000000000 ) ) ;
#16604=CIRCLE ( 'NONE', #4156, 8.000000000000000000 ) ;
#16608=VERTEX_POINT ( 'NONE', #11717 ) ;
#16615=LINE ( 'NONE', #11462, #15122 ) ;
#16619=CARTESIAN_POINT ( 'NONE',  ( 43.99999999999999289, 50.99999999999999289, 0.5000000000000000000 ) ) ;
#16621=VECTOR ( 'NONE', #13947, 1000.000000000000000 ) ;
#16636=VECTOR ( 'NONE', #20605, 1000.000000000000000 ) ;
#16644=FACE_OUTER_BOUND ( 'NONE', #8988, .T. ) ;
#16652=DIRECTION ( 'NONE',  ( 1.000000000000000000, 0.000000000000000000, 0.000000000000000000 ) ) ;
#16656=VERTEX_POINT ( 'NONE', #8451 ) ;
#16657=DIRECTION ( 'NONE',  ( -0.000000000000000000, -0.000000000000000000, -1.000000000000000000 ) ) ;
#16665=VERTEX_POINT ( 'NONE', #6628 ) ;
#16676=EDGE_CURVE ( 'NONE', #18123, #22195, #23466, .T. ) ;
#16680=CARTESIAN_POINT ( 'NONE',  ( -28.73477696352898292, -42.73830357953205805, -1.500000000000000000 ) ) ;
#16704=DIRECTION ( 'NONE',  ( -1.000000000000000000, 0.000000000000000000, 0.000000000000000000 ) ) ;
#16709=DIRECTION ( 'NONE',  ( 1.000000000000000000, 0.000000000000000000, 0.000000000000000000 ) ) ;
#16718=EDGE_LOOP ( 'NONE', ( #20322, #5756, #7826, #11120 ) ) ;
#16724=ORIENTED_EDGE ( 'NONE', *, *, #18738, .F. ) ;
#16725=CARTESIAN_POINT ( 'NONE',  ( 43.99999999999999289, 50.99999999999999289, 0.5000000000000000000 ) ) ;
#16731=DIRECTION ( 'NONE',  ( 0.7089874389501501506, -0.7052211081716905916, 0.000000000000000000 ) ) ;
#16736=ORIENTED_EDGE ( 'NONE', *, *, #9348, .T. ) ;
#16737=AXIS2_PLACEMENT_3D ( 'NONE', #9256, #10948, #18199 ) ;
#16747=CARTESIAN_POINT ( 'NONE',  ( 3.890962118697714531E-15, 15.50000000000000000, 12.50000000000000000 ) ) ;
#16750=DIRECTION ( 'NONE',  ( -0.000000000000000000, -0.000000000000000000, -1.000000000000000000 ) ) ;
#16751=DIRECTION ( 'NONE',  ( 0.5579568342432839056, 0.8298699724180966797, 0.000000000000000000 ) ) ;
#16753=ORIENTED_EDGE ( 'NONE', *, *, #2010, .T. ) ;
#16755=EDGE_CURVE ( 'NONE', #17856, #13312, #20277, .T. ) ;
#16759=ORIENTED_EDGE ( 'NONE', *, *, #15224, .F. ) ;
#16760=VERTEX_POINT ( 'NONE', #22233 ) ;
#16769=DIRECTION ( 'NONE',  ( 0.7089874389501501506, 0.7052211081716905916, 0.000000000000000000 ) ) ;
#16781=CARTESIAN_POINT ( 'NONE',  ( 0.000000000000000000, 45.00000000000000000, -3.000000000000000000 ) ) ;
#16792=DIRECTION ( 'NONE',  ( 0.000000000000000000, -1.000000000000000000, 0.000000000000000000 ) ) ;
#16800=CIRCLE ( 'NONE', #12927, 1.500000000000000000 ) ;
#16804=DIRECTION ( 'NONE',  ( -0.000000000000000000, -0.000000000000000000, -1.000000000000000000 ) ) ;
#16809=ORIENTED_EDGE ( 'NONE', *, *, #6233, .T. ) ;
#16810=EDGE_CURVE ( 'NONE', #13616, #47, #3552, .T. ) ;
#16811=EDGE_LOOP ( 'NONE', ( #23893, #19816 ) ) ;
#16824=CIRCLE ( 'NONE', #7866, 1.499999999999994449 ) ;
#16836=EDGE_CURVE ( 'NONE', #23135, #3028, #599, .T. ) ;
#16837=PLANE ( 'NONE',  #10994 ) ;
#16838=AXIS2_PLACEMENT_3D ( 'NONE', #1931, #11062, #14490 ) ;
#16842=ORIENTED_EDGE ( 'NONE', *, *, #22417, .T. ) ;
#16865=CIRCLE ( 'NONE', #21171, 8.000000000000000000 ) ;
#16866=ORIENTED_EDGE ( 'NONE', *, *, #18346, .T. ) ;
#16868=LINE ( 'NONE', #9549, #17598 ) ;
#16870=CARTESIAN_POINT ( 'NONE',  ( -33.24999999999999289, 29.50000000000000000, -3.000000000000000000 ) ) ;
#16872=ORIENTED_EDGE ( 'NONE', *, *, #19540, .T. ) ;
#16878=VERTEX_POINT ( 'NONE', #12031 ) ;
#16888=EDGE_LOOP ( 'NONE', ( #5445, #15717, #18105, #23943 ) ) ;
#16890=CARTESIAN_POINT ( 'NONE',  ( -28.99999999999999645, 29.50000000000000000, -3.000000000000000000 ) ) ;
#16916=EDGE_CURVE ( 'NONE', #747, #19039, #16373, .T. ) ;
#16920=EDGE_LOOP ( 'NONE', ( #6013, #19124, #6412, #17546 ) ) ;
#16928=CARTESIAN_POINT ( 'NONE',  ( -28.99999999999998579, -29.50000000000000711, 0.000000000000000000 ) ) ;
#16929=LINE ( 'NONE', #13524, #22835 ) ;
#16934=ORIENTED_EDGE ( 'NONE', *, *, #1253, .T. ) ;
#16947=CONICAL_SURFACE ( 'NONE', #22799, 39.49999999999999289, 0.7853981633974621568 ) ;
#16959=AXIS2_PLACEMENT_3D ( 'NONE', #12928, #16599, #12696 ) ;
#16961=AXIS2_PLACEMENT_3D ( 'NONE', #1540, #18607, #2148 ) ;
#16967=CARTESIAN_POINT ( 'NONE',  ( 42.00000000000000000, 25.22443390181681622, -1.500000000000000000 ) ) ;
#16968=CARTESIAN_POINT ( 'NONE',  ( 44.99999999999998579, 50.99999999999992184, 0.000000000000000000 ) ) ;
#16974=CARTESIAN_POINT ( 'NONE',  ( 34.02499999999999858, 29.50000000000000000, -3.000000000000000000 ) ) ;
#16975=DIRECTION ( 'NONE',  ( -1.000000000000000000, -1.387778780781445478E-15, 0.000000000000000000 ) ) ;
#16976=CYLINDRICAL_SURFACE ( 'NONE', #18573, 8.000000000000000000 ) ;
#16986=ADVANCED_FACE ( 'NONE', ( #20527 ), #3800, .F. ) ;
#16991=EDGE_CURVE ( 'NONE', #23864, #1818, #19280, .T. ) ;
#16993=DIRECTION ( 'NONE',  ( 0.8298699724180977899, 0.5579568342432823513, -0.000000000000000000 ) ) ;
#16994=ORIENTED_EDGE ( 'NONE', *, *, #15623, .F. ) ;
#17001=LINE ( 'NONE', #7593, #15726 ) ;
#17007=CARTESIAN_POINT ( 'NONE',  ( 28.73477696352899713, 42.73830357953205095, -1.500000000000000000 ) ) ;
#17010=ORIENTED_EDGE ( 'NONE', *, *, #22569, .T. ) ;
#17011=CIRCLE ( 'NONE', #8452, 4.249999999999996447 ) ;
#17020=ORIENTED_EDGE ( 'NONE', *, *, #15576, .F. ) ;
#17021=CARTESIAN_POINT ( 'NONE',  ( -36.00000000000000711, -51.00000000000000711, 0.000000000000000000 ) ) ;
#17029=ORIENTED_EDGE ( 'NONE', *, *, #14382, .T. ) ;
#17032=CARTESIAN_POINT ( 'NONE',  ( -40.66734255040736201, -26.56420859267092283, -3.000000000000000000 ) ) ;
#17060=AXIS2_PLACEMENT_3D ( 'NONE', #11639, #1908, #9797 ) ;
#17061=DIRECTION ( 'NONE',  ( -0.7071067811865292541, 0.000000000000000000, -0.7071067811865658914 ) ) ;
#17065=EDGE_LOOP ( 'NONE', ( #46, #24095, #14423, #10597 ) ) ;
#17067=ORIENTED_EDGE ( 'NONE', *, *, #19184, .T. ) ;
#17068=ADVANCED_FACE ( 'NONE', ( #11402 ), #22652, .F. ) ;
#17078=FACE_OUTER_BOUND ( 'NONE', #14703, .T. ) ;
#17080=ORIENTED_EDGE ( 'NONE', *, *, #2903, .T. ) ;
#17088=CARTESIAN_POINT ( 'NONE',  ( 40.23082370883258818, -29.49999999999999645, -3.000000000000000000 ) ) ;
#17097=EDGE_LOOP ( 'NONE', ( #4141, #21241, #19078, #583 ) ) ;
#17120=AXIS2_PLACEMENT_3D ( 'NONE', #21445, #4365, #11778 ) ;
#17125=EDGE_CURVE ( 'NONE', #14863, #23135, #23019, .T. ) ;
#17146=PLANE ( 'NONE',  #9372 ) ;
#17151=DIRECTION ( 'NONE',  ( -0.000000000000000000, -0.000000000000000000, 1.000000000000000000 ) ) ;
#17153=ORIENTED_EDGE ( 'NONE', *, *, #14141, .F. ) ;
#17163=CARTESIAN_POINT ( 'NONE',  ( 40.23082370883260239, 29.49999999999999645, -3.000000000000000000 ) ) ;
#17185=DIRECTION ( 'NONE',  ( 0.000000000000000000, 0.000000000000000000, 1.000000000000000000 ) ) ;
#17186=DIRECTION ( 'NONE',  ( 0.000000000000000000, 0.000000000000000000, 1.000000000000000000 ) ) ;
#17203=DIRECTION ( 'NONE',  ( -1.000000000000000000, 0.000000000000000000, 0.000000000000000000 ) ) ;
#17213=ADVANCED_FACE ( 'NONE', ( #12130 ), #19607, .F. ) ;
#17220=ORIENTED_EDGE ( 'NONE', *, *, #20097, .T. ) ;
#17224=AXIS2_PLACEMENT_3D ( 'NONE', #22186, #20115, #23768 ) ;
#17230=CARTESIAN_POINT ( 'NONE',  ( 35.99999999999999289, -51.00000000000000711, 0.5000000000000000000 ) ) ;
#17232=ADVANCED_FACE ( 'NONE', ( #13620 ), #23151, .T. ) ;
#17233=ORIENTED_EDGE ( 'NONE', *, *, #22227, .T. ) ;
#17236=FACE_OUTER_BOUND ( 'NONE', #22273, .T. ) ;
#17238=CARTESIAN_POINT ( 'NONE',  ( 43.50000000000000711, 25.84341543330623026, 0.000000000000000000 ) ) ;
#17241=FACE_OUTER_BOUND ( 'NONE', #18080, .T. ) ;
#17248=VECTOR ( 'NONE', #3141, 1000.000000000000000 ) ;
#17256=DIRECTION ( 'NONE',  ( -1.000000000000000000, 0.000000000000000000, 0.000000000000000000 ) ) ;
#17267=AXIS2_PLACEMENT_3D ( 'NONE', #5760, #21790, #7679 ) ;
#17268=VECTOR ( 'NONE', #333, 999.9999999999998863 ) ;
#17269=EDGE_LOOP ( 'NONE', ( #19198, #12863 ) ) ;
#17272=AXIS2_PLACEMENT_3D ( 'NONE', #11864, #14184, #6755 ) ;
#17276=AXIS2_PLACEMENT_3D ( 'NONE', #12744, #20205, #10894 ) ;
#17312=AXIS2_PLACEMENT_3D ( 'NONE', #11706, #4563, #19313 ) ;
#17313=ORIENTED_EDGE ( 'NONE', *, *, #6379, .F. ) ;
#17319=CARTESIAN_POINT ( 'NONE',  ( -44.00000000000000711, -51.00000000000000711, 0.5000000000000000000 ) ) ;
#17322=DIRECTION ( 'NONE',  ( -0.000000000000000000, -0.000000000000000000, -1.000000000000000000 ) ) ;
#17331=FACE_OUTER_BOUND ( 'NONE', #5120, .T. ) ;
#17335=CARTESIAN_POINT ( 'NONE',  ( -36.00000000000001421, 50.99999999999999289, 0.5000000000000000000 ) ) ;
#17338=CARTESIAN_POINT ( 'NONE',  ( 24.75000000000000711, -29.50000000000000000, -3.000000000000000000 ) ) ;
#17353=DIRECTION ( 'NONE',  ( -1.000000000000000000, 0.000000000000000000, 0.000000000000000000 ) ) ;
#17356=VECTOR ( 'NONE', #871, 1000.000000000000000 ) ;
#17370=DIRECTION ( 'NONE',  ( -0.000000000000000000, -0.000000000000000000, -1.000000000000000000 ) ) ;
#17375=ORIENTED_EDGE ( 'NONE', *, *, #5668, .T. ) ;
#17376=AXIS2_PLACEMENT_3D ( 'NONE', #24082, #20424, #12613 ) ;
#17378=CONICAL_SURFACE ( 'NONE', #15008, 4.249999999999996447, 1.029744258676654090 ) ;
#17381=EDGE_LOOP ( 'NONE', ( #13686, #21588, #17153 ) ) ;
#17382=VERTEX_POINT ( 'NONE', #22160 ) ;
#17383=ORIENTED_EDGE ( 'NONE', *, *, #12616, .F. ) ;
#17384=EDGE_CURVE ( 'NONE', #5799, #5565, #1329, .T. ) ;
#17400=CIRCLE ( 'NONE', #9596, 1.499999999999994449 ) ;
#17402=ORIENTED_EDGE ( 'NONE', *, *, #19300, .F. ) ;
#17422=EDGE_CURVE ( 'NONE', #10822, #17524, #22756, .T. ) ;
#17437=ORIENTED_EDGE ( 'NONE', *, *, #10942, .T. ) ;
#17441=EDGE_CURVE ( 'NONE', #5565, #1549, #5603, .T. ) ;
#17449=EDGE_LOOP ( 'NONE', ( #5169, #927, #995, #15916 ) ) ;
#17450=FACE_OUTER_BOUND ( 'NONE', #23625, .T. ) ;
#17451=DIRECTION ( 'NONE',  ( -0.7052211081716897034, -0.7089874389501510388, 0.000000000000000000 ) ) ;
#17459=ORIENTED_EDGE ( 'NONE', *, *, #11333, .F. ) ;
#17470=VERTEX_POINT ( 'NONE', #20925 ) ;
#17476=FACE_BOUND ( 'NONE', #8179, .T. ) ;
#17484=FACE_OUTER_BOUND ( 'NONE', #11267, .T. ) ;
#17488=VERTEX_POINT ( 'NONE', #18718 ) ;
#17491=ORIENTED_EDGE ( 'NONE', *, *, #22099, .T. ) ;
#17511=CARTESIAN_POINT ( 'NONE',  ( -36.00000000000000711, -51.00000000000000711, 0.000000000000000000 ) ) ;
#17513=DIRECTION ( 'NONE',  ( 1.000000000000000000, 0.000000000000000000, 0.000000000000000000 ) ) ;
#17522=EDGE_CURVE ( 'NONE', #6942, #17856, #3722, .T. ) ;
#17524=VERTEX_POINT ( 'NONE', #11135 ) ;
#17529=FACE_OUTER_BOUND ( 'NONE', #10239, .T. ) ;
#17533=FACE_OUTER_BOUND ( 'NONE', #11346, .T. ) ;
#17540=FACE_OUTER_BOUND ( 'NONE', #20296, .T. ) ;
#17542=DIRECTION ( 'NONE',  ( -5.501724186093585079E-16, -1.000000000000000000, 0.000000000000000000 ) ) ;
#17545=EDGE_CURVE ( 'NONE', #17470, #12988, #22265, .T. ) ;
#17546=ORIENTED_EDGE ( 'NONE', *, *, #3764, .F. ) ;
#17550=ADVANCED_FACE ( 'NONE', ( #6031 ), #20797, .F. ) ;
#17551=ORIENTED_EDGE ( 'NONE', *, *, #4550, .T. ) ;
#17559=CYLINDRICAL_SURFACE ( 'NONE', #11743, 8.999999999999994671 ) ;
#17562=DIRECTION ( 'NONE',  ( 0.7089874389501514829, -0.7052211081716890373, 0.000000000000000000 ) ) ;
#17564=CARTESIAN_POINT ( 'NONE',  ( 41.73082370883260239, 27.62204025492844650, 0.000000000000000000 ) ) ;
#17566=ADVANCED_FACE ( 'NONE', ( #420 ), #11619, .F. ) ;
#17573=CARTESIAN_POINT ( 'NONE',  ( 30.32370777929697780, -42.16181938034194587, 0.000000000000000000 ) ) ;
#17580=CIRCLE ( 'NONE', #13284, 4.499999999999997335 ) ;
#17582=ORIENTED_EDGE ( 'NONE', *, *, #15829, .T. ) ;
#17584=DIRECTION ( 'NONE',  ( -0.000000000000000000, -0.000000000000000000, -1.000000000000000000 ) ) ;
#17587=ORIENTED_EDGE ( 'NONE', *, *, #5495, .T. ) ;
#17592=CARTESIAN_POINT ( 'NONE',  ( 29.00000000000000000, 29.50000000000000000, 14.00000000000000178 ) ) ;
#17598=VECTOR ( 'NONE', #15039, 1000.000000000000000 ) ;
#17602=DIRECTION ( 'NONE',  ( 0.000000000000000000, 0.000000000000000000, 1.000000000000000000 ) ) ;
#17603=DIRECTION ( 'NONE',  ( -1.000000000000000000, 0.000000000000000000, 0.000000000000000000 ) ) ;
#17616=AXIS2_PLACEMENT_3D ( 'NONE', #2439, #17322, #22951 ) ;
#17629=EDGE_CURVE ( 'NONE', #15211, #21933, #6790, .T. ) ;
#17630=FACE_OUTER_BOUND ( 'NONE', #17449, .T. ) ;
#17658=ORIENTED_EDGE ( 'NONE', *, *, #11736, .F. ) ;
#17664=EDGE_CURVE ( 'NONE', #14048, #19008, #8196, .T. ) ;
#17666=EDGE_CURVE ( 'NONE', #23706, #16325, #10146, .T. ) ;
#17673=ORIENTED_EDGE ( 'NONE', *, *, #9392, .F. ) ;
#17684=CARTESIAN_POINT ( 'NONE',  ( 33.25000000000000000, 29.50000000000000000, -3.000000000000000000 ) ) ;
#17686=DIRECTION ( 'NONE',  ( -1.000000000000000000, 0.000000000000000000, 0.000000000000000000 ) ) ;
#17693=DIRECTION ( 'NONE',  ( 0.000000000000000000, 1.000000000000000000, -0.000000000000000000 ) ) ;
#17703=CARTESIAN_POINT ( 'NONE',  ( -36.00000000000001421, 50.99999999999999289, 0.000000000000000000 ) ) ;
#17710=AXIS2_PLACEMENT_3D ( 'NONE', #12408, #21703, #21343 ) ;
#17712=DIRECTION ( 'NONE',  ( -0.000000000000000000, -0.000000000000000000, -1.000000000000000000 ) ) ;
#17718=AXIS2_PLACEMENT_3D ( 'NONE', #3979, #7855, #18636 ) ;
#17719=AXIS2_PLACEMENT_3D ( 'NONE', #1495, #23699, #7072 ) ;
#17725=ORIENTED_EDGE ( 'NONE', *, *, #7246, .F. ) ;
#17726=CIRCLE ( 'NONE', #23596, 1.999999999999996669 ) ;
#17727=VERTEX_POINT ( 'NONE', #4586 ) ;
#17739=ORIENTED_EDGE ( 'NONE', *, *, #7425, .F. ) ;
#17741=FACE_OUTER_BOUND ( 'NONE', #6993, .T. ) ;
#17742=FACE_OUTER_BOUND ( 'NONE', #7773, .T. ) ;
#17749=ADVANCED_FACE ( 'NONE', ( #17741 ), #19709, .F. ) ;
#17750=TOROIDAL_SURFACE ( 'NONE', #4565, 3.500000000000001776, 1.500000000000000000 ) ;
#17754=ORIENTED_EDGE ( 'NONE', *, *, #17664, .T. ) ;
#17763=ADVANCED_FACE ( 'NONE', ( #9775 ), #543, .F. ) ;
#17777=CARTESIAN_POINT ( 'NONE',  ( 23.97500000000000497, 29.50000000000000000, -3.000000000000000000 ) ) ;
#17781=ORIENTED_EDGE ( 'NONE', *, *, #10015, .F. ) ;
#17790=ORIENTED_EDGE ( 'NONE', *, *, #19185, .F. ) ;
#17799=ORIENTED_EDGE ( 'NONE', *, *, #23686, .F. ) ;
#17806=DIRECTION ( 'NONE',  ( 1.000000000000000000, 0.000000000000000000, 0.000000000000000000 ) ) ;
#17807=VECTOR ( 'NONE', #19718, 1000.000000000000114 ) ;
#17812=VERTEX_POINT ( 'NONE', #1404 ) ;
#17843=ORIENTED_EDGE ( 'NONE', *, *, #20615, .T. ) ;
#17856=VERTEX_POINT ( 'NONE', #8821 ) ;
#17868=ORIENTED_EDGE ( 'NONE', *, *, #8108, .F. ) ;
#17877=EDGE_CURVE ( 'NONE', #1091, #747, #18337, .T. ) ;
#17879=ORIENTED_EDGE ( 'NONE', *, *, #19788, .T. ) ;
#17883=CARTESIAN_POINT ( 'NONE',  ( -14.99999999999999645, 15.50000000000000178, 14.70000000000000284 ) ) ;
#17892=DIRECTION ( 'NONE',  ( 0.7071067811865474617, 8.659560562354932858E-17, -0.7071067811865474617 ) ) ;
#17900=VERTEX_POINT ( 'NONE', #13301 ) ;
#17905=ORIENTED_EDGE ( 'NONE', *, *, #22266, .F. ) ;
#17908=ORIENTED_EDGE ( 'NONE', *, *, #1857, .T. ) ;
#17910=DIRECTION ( 'NONE',  ( -0.000000000000000000, -0.000000000000000000, 1.000000000000000000 ) ) ;
#17916=SPHERICAL_SURFACE ( 'NONE', #21928, 1.500000000000000000 ) ;
#17919=EDGE_CURVE ( 'NONE', #22424, #4863, #9172, .T. ) ;
#17922=ORIENTED_EDGE ( 'NONE', *, *, #712, .T. ) ;
#17926=EDGE_CURVE ( 'NONE', #19039, #6856, #14895, .T. ) ;
#17938=CARTESIAN_POINT ( 'NONE',  ( 41.73082370883258108, -27.62204025492843940, -1.500000000000000000 ) ) ;
#17942=ORIENTED_EDGE ( 'NONE', *, *, #3764, .T. ) ;
#17944=VERTEX_POINT ( 'NONE', #7568 ) ;
#17948=DIRECTION ( 'NONE',  ( 1.000000000000000000, 0.000000000000000000, 0.000000000000000000 ) ) ;
#17955=VERTEX_POINT ( 'NONE', #16974 ) ;
#17971=DIRECTION ( 'NONE',  ( 0.000000000000000000, 0.000000000000000000, 1.000000000000000000 ) ) ;
#17976=ADVANCED_FACE ( 'NONE', ( #3924 ), #1965, .F. ) ;
#17988=ORIENTED_EDGE ( 'NONE', *, *, #4288, .T. ) ;
#17999=CARTESIAN_POINT ( 'NONE',  ( 40.23082370883260239, 29.49999999999999645, -3.000000000000000000 ) ) ;
#18013=AXIS2_PLACEMENT_3D ( 'NONE', #16311, #8394, #23307 ) ;
#18017=VECTOR ( 'NONE', #4942, 1000.000000000000000 ) ;
#18027=DIRECTION ( 'NONE',  ( -0.000000000000000000, -0.000000000000000000, -1.000000000000000000 ) ) ;
#18031=AXIS2_PLACEMENT_3D ( 'NONE', #9010, #23916, #7191 ) ;
#18032=LINE ( 'NONE', #1332, #14121 ) ;
#18039=AXIS2_PLACEMENT_3D ( 'NONE', #20634, #9511, #501 ) ;
#18044=ORIENTED_EDGE ( 'NONE', *, *, #11214, .T. ) ;
#18070=DIRECTION ( 'NONE',  ( -0.000000000000000000, -0.000000000000000000, -1.000000000000000000 ) ) ;
#18076=TOROIDAL_SURFACE ( 'NONE', #11416, 12.73082370883260417, 1.500000000000000000 ) ;
#18080=EDGE_LOOP ( 'NONE', ( #2310, #9421, #8751, #5358 ) ) ;
#18089=DIRECTION ( 'NONE',  ( -1.000000000000000000, 0.000000000000000000, 0.000000000000000000 ) ) ;
#18094=EDGE_CURVE ( 'NONE', #15532, #8263, #9737, .T. ) ;
#18104=AXIS2_PLACEMENT_3D ( 'NONE', #12653, #14470, #18167 ) ;
#18105=ORIENTED_EDGE ( 'NONE', *, *, #20979, .F. ) ;
#18114=AXIS2_PLACEMENT_3D ( 'NONE', #574, #7748, #5577 ) ;
#18118=VECTOR ( 'NONE', #21554, 1000.000000000000000 ) ;
#18123=VERTEX_POINT ( 'NONE', #19064 ) ;
#18127=DIRECTION ( 'NONE',  ( 0.000000000000000000, 0.000000000000000000, 1.000000000000000000 ) ) ;
#18130=ORIENTED_EDGE ( 'NONE', *, *, #14084, .T. ) ;
#18136=LINE ( 'NONE', #1429, #21813 ) ;
#18137=DIRECTION ( 'NONE',  ( -0.000000000000000000, -0.000000000000000000, 1.000000000000000000 ) ) ;
#18138=DIRECTION ( 'NONE',  ( -0.000000000000000000, -0.000000000000000000, -1.000000000000000000 ) ) ;
#18139=DIRECTION ( 'NONE',  ( -0.1039766011667100087, 0.9945797436152714610, 0.000000000000000000 ) ) ;
#18144=EDGE_LOOP ( 'NONE', ( #545, #2229, #18964, #11049 ) ) ;
#18162=EDGE_LOOP ( 'NONE', ( #11547, #14432 ) ) ;
#18167=DIRECTION ( 'NONE',  ( -1.000000000000000000, 0.000000000000000000, 0.000000000000000000 ) ) ;
#18174=ORIENTED_EDGE ( 'NONE', *, *, #5638, .F. ) ;
#18184=CYLINDRICAL_SURFACE ( 'NONE', #10576, 11.23082370883260417 ) ;
#18185=FACE_OUTER_BOUND ( 'NONE', #15965, .T. ) ;
#18198=DIRECTION ( 'NONE',  ( -0.000000000000000000, -0.000000000000000000, -1.000000000000000000 ) ) ;
#18199=DIRECTION ( 'NONE',  ( 1.000000000000000000, 0.000000000000000000, 0.000000000000000000 ) ) ;
#18210=EDGE_CURVE ( 'NONE', #17470, #14876, #11675, .T. ) ;
#18213=VERTEX_POINT ( 'NONE', #17573 ) ;
#18217=ORIENTED_EDGE ( 'NONE', *, *, #9987, .F. ) ;
#18223=PRODUCT ( 'Drive End Plate', 'Drive End Plate', '', ( #10675 ) ) ;
#18233=AXIS2_PLACEMENT_3D ( 'NONE', #10511, #17971, #14300 ) ;
#18238=ORIENTED_EDGE ( 'NONE', *, *, #7494, .T. ) ;
#18240=DIRECTION ( 'NONE',  ( -1.000000000000000000, 0.000000000000000000, 0.000000000000000000 ) ) ;
#18262=CARTESIAN_POINT ( 'NONE',  ( -31.50000000000001421, 50.99999999999999289, 12.50000000000000000 ) ) ;
#18265=CARTESIAN_POINT ( 'NONE',  ( -30.68762588338046982, -45.64284848299540442, -3.000000000000000000 ) ) ;
#18273=DIRECTION ( 'NONE',  ( -0.000000000000000000, -0.000000000000000000, 1.000000000000000000 ) ) ;
#18274=ORIENTED_EDGE ( 'NONE', *, *, #4675, .F. ) ;
#18281=VERTEX_POINT ( 'NONE', #10701 ) ;
#18287=VERTEX_POINT ( 'NONE', #18526 ) ;
#18293=DIRECTION ( 'NONE',  ( -1.000000000000000000, 0.000000000000000000, 0.000000000000000000 ) ) ;
#18299=ORIENTED_EDGE ( 'NONE', *, *, #21444, .F. ) ;
#18303=DIRECTION ( 'NONE',  ( -1.000000000000000000, 0.000000000000000000, 0.000000000000000000 ) ) ;
#18309=EDGE_CURVE ( 'NONE', #23706, #11173, #3156, .T. ) ;
#18312=VERTEX_POINT ( 'NONE', #18750 ) ;
#18326=DIRECTION ( 'NONE',  ( -0.000000000000000000, -0.000000000000000000, 1.000000000000000000 ) ) ;
#18333=CARTESIAN_POINT ( 'NONE',  ( -42.00000000000000000, 25.22443390181683043, -3.000000000000000000 ) ) ;
#18337=LINE ( 'NONE', #5055, #9489 ) ;
#18340=CARTESIAN_POINT ( 'NONE',  ( 0.000000000000000000, 45.00000000000000000, -8.673617379884035472E-16 ) ) ;
#18344=VERTEX_POINT ( 'NONE', #15184 ) ;
#18346=EDGE_CURVE ( 'NONE', #22249, #18312, #20593, .T. ) ;
#18352=CARTESIAN_POINT ( 'NONE',  ( 3.890962118697714531E-15, 15.50000000000000000, 14.70000000000000284 ) ) ;
#18353=CARTESIAN_POINT ( 'NONE',  ( 3.890962118697714531E-15, 15.50000000000000000, 7.700000000000001954 ) ) ;
#18359=DIRECTION ( 'NONE',  ( -1.360567432138674546E-16, 1.000000000000000000, 0.000000000000000000 ) ) ;
#18362=DIRECTION ( 'NONE',  ( -0.000000000000000000, -0.000000000000000000, -1.000000000000000000 ) ) ;
#18364=MANIFOLD_SOLID_BREP ( '\X2\00d8\X0\4.0mm Dowel Hole1', #3847 ) ;
#18373=DIRECTION ( 'NONE',  ( 0.9945797436152712390, -0.1039766011667123125, -2.300427773307206454E-15 ) ) ;
#18377=DIRECTION ( 'NONE',  ( -0.000000000000000000, -0.000000000000000000, 1.000000000000000000 ) ) ;
#18384=ORIENTED_EDGE ( 'NONE', *, *, #22382, .T. ) ;
#18390=CIRCLE ( 'NONE', #14533, 1.500000000000000222 ) ;
#18399=EDGE_LOOP ( 'NONE', ( #15901, #19689 ) ) ;
#18400=EDGE_LOOP ( 'NONE', ( #2346, #3529 ) ) ;
#18403=CARTESIAN_POINT ( 'NONE',  ( -28.99999999999999645, -29.50000000000000000, -3.000000000000000000 ) ) ;
#18408=FACE_OUTER_BOUND ( 'NONE', #10849, .T. ) ;
#18411=AXIS2_PLACEMENT_3D ( 'NONE', #11428, #22932, #11669 ) ;
#18413=AXIS2_PLACEMENT_3D ( 'NONE', #20357, #8892, #9347 ) ;
#18417=CARTESIAN_POINT ( 'NONE',  ( -41.73082370883257397, -27.62204025492845361, -3.000000000000000000 ) ) ;
#18428=AXIS2_PLACEMENT_3D ( 'NONE', #3533, #18070, #7311 ) ;
#18432=CARTESIAN_POINT ( 'NONE',  ( 41.99999999999997868, -25.22443390181679845, -0.6213203435596419411 ) ) ;
#18439=VECTOR ( 'NONE', #205, 1000.000000000000000 ) ;
#18440=DIRECTION ( 'NONE',  ( -1.000000000000000000, 0.000000000000000000, 0.000000000000000000 ) ) ;
#18447=DIRECTION ( 'NONE',  ( 1.000000000000000000, 0.000000000000000000, 0.000000000000000000 ) ) ;
#18457=DIRECTION ( 'NONE',  ( 0.000000000000000000, 0.000000000000000000, -1.000000000000000000 ) ) ;
#18459=ORIENTED_EDGE ( 'NONE', *, *, #4163, .F. ) ;
#18464=ORIENTED_EDGE ( 'NONE', *, *, #17926, .F. ) ;
#18471=ADVANCED_FACE ( 'NONE', ( #8369 ), #8591, .F. ) ;
#18475=ORIENTED_EDGE ( 'NONE', *, *, #15339, .F. ) ;
#18476=VECTOR ( 'NONE', #11430, 1000.000000000000000 ) ;
#18481=FACE_BOUND ( 'NONE', #15533, .T. ) ;
#18483=FACE_BOUND ( 'NONE', #14323, .T. ) ;
#18485=CYLINDRICAL_SURFACE ( 'NONE', #3261, 4.499999999999997335 ) ;
#18508=CARTESIAN_POINT ( 'NONE',  ( 31.49999999999999289, -51.00000000000000711, 12.50000000000000000 ) ) ;
#18509=CARTESIAN_POINT ( 'NONE',  ( 10.00000000000000533, 15.50000000000000000, 7.699999999999998401 ) ) ;
#18525=ADVANCED_FACE ( 'NONE', ( #7019 ), #7059, .F. ) ;
#18526=CARTESIAN_POINT ( 'NONE',  ( 1.999999999999997113, 45.00000000000000000, -2.974999999999996092 ) ) ;
#18528=ORIENTED_EDGE ( 'NONE', *, *, #3289, .T. ) ;
#18535=AXIS2_PLACEMENT_3D ( 'NONE', #20384, #10739, #10853 ) ;
#18539=VECTOR ( 'NONE', #6554, 1000.000000000000000 ) ;
#18543=CARTESIAN_POINT ( 'NONE',  ( -28.99999999999999645, -29.50000000000000000, 12.50000000000000000 ) ) ;
#18552=LINE ( 'NONE', #14390, #7388 ) ;
#18565=ADVANCED_FACE ( 'NONE', ( #1519 ), #22657, .F. ) ;
#18572=VECTOR ( 'NONE', #6651, 1000.000000000000000 ) ;
#18573=AXIS2_PLACEMENT_3D ( 'NONE', #7692, #15130, #648 ) ;
#18575=EDGE_LOOP ( 'NONE', ( #18595, #21918, #12526, #13582 ) ) ;
#18583=CARTESIAN_POINT ( 'NONE',  ( -28.99999999999999645, 29.50000000000000000, -3.000000000000000000 ) ) ;
#18595=ORIENTED_EDGE ( 'NONE', *, *, #2291, .T. ) ;
#18597=EDGE_LOOP ( 'NONE', ( #23661, #11878 ) ) ;
#18599=DIRECTION ( 'NONE',  ( 0.000000000000000000, 0.000000000000000000, 1.000000000000000000 ) ) ;
#18601=DIRECTION ( 'NONE',  ( -0.000000000000000000, -1.000000000000000000, -0.000000000000000000 ) ) ;
#18602=VERTEX_POINT ( 'NONE', #3341 ) ;
#18606=FACE_BOUND ( 'NONE', #18399, .T. ) ;
#18607=DIRECTION ( 'NONE',  ( -0.000000000000000000, -0.000000000000000000, 1.000000000000000000 ) ) ;
#18610=DIRECTION ( 'NONE',  ( -1.000000000000000000, 0.000000000000000000, 0.000000000000000000 ) ) ;
#18636=DIRECTION ( 'NONE',  ( -1.000000000000000000, 0.000000000000000000, 0.000000000000000000 ) ) ;
#18647=ORIENTED_EDGE ( 'NONE', *, *, #7255, .T. ) ;
#18648=AXIS2_PLACEMENT_3D ( 'NONE', #22506, #13205, #22387 ) ;
#18668=EDGE_LOOP ( 'NONE', ( #2004, #312, #20418, #17658 ) ) ;
#18677=DIRECTION ( 'NONE',  ( -1.000000000000000000, 0.000000000000000000, 0.000000000000000000 ) ) ;
#18696=LINE ( 'NONE', #15384, #15052 ) ;
#18708=EDGE_CURVE ( 'NONE', #22066, #8450, #16105, .T. ) ;
#18713=CYLINDRICAL_SURFACE ( 'NONE', #9046, 1.499999999999994449 ) ;
#18715=CARTESIAN_POINT ( 'NONE',  ( 39.50000000000000000, 15.50000000000000533, 19.70000000000000284 ) ) ;
#18718=CARTESIAN_POINT ( 'NONE',  ( 43.99999999999999289, 50.99999999999999289, 0.000000000000000000 ) ) ;
#18728=ORIENTED_EDGE ( 'NONE', *, *, #15421, .T. ) ;
#18732=MECHANICAL_DESIGN_GEOMETRIC_PRESENTATION_REPRESENTATION('',(#10923),#11300);
#18735=DIRECTION ( 'NONE',  ( -1.000000000000000000, 0.000000000000000000, 0.000000000000000000 ) ) ;
#18738=EDGE_CURVE ( 'NONE', #12662, #1759, #15983, .T. ) ;
#18750=CARTESIAN_POINT ( 'NONE',  ( 40.66734255040735491, -26.56420859267090862, -1.500000000000000000 ) ) ;
#18751=ORIENTED_EDGE ( 'NONE', *, *, #7438, .F. ) ;
#18758=DIRECTION ( 'NONE',  ( -0.000000000000000000, -0.000000000000000000, -1.000000000000000000 ) ) ;
#18779=CARTESIAN_POINT ( 'NONE',  ( 17.25000000000000000, 15.50000000000000178, 16.70000000000000284 ) ) ;
#18784=ADVANCED_FACE ( 'NONE', ( #17450 ), #23069, .F. ) ;
#18793=DIRECTION ( 'NONE',  ( -0.1039766011667100087, 0.9945797436152714610, 0.000000000000000000 ) ) ;
#18800=CARTESIAN_POINT ( 'NONE',  ( -14.99999999999999645, 15.50000000000000178, 16.70000000000000284 ) ) ;
#18814=CONICAL_SURFACE ( 'NONE', #5967, 2.024999999999999911, 0.7853981633974222998 ) ;
#18818=ADVANCED_FACE ( 'NONE', ( #3652 ), #8895, .F. ) ;
#18822=ORIENTED_EDGE ( 'NONE', *, *, #8671, .F. ) ;
#18827=DIRECTION ( 'NONE',  ( 1.000000000000000000, 0.000000000000000000, 0.000000000000000000 ) ) ;
#18829=VECTOR ( 'NONE', #3558, 1000.000000000000000 ) ;
#18831=CARTESIAN_POINT ( 'NONE',  ( 0.000000000000000000, 0.000000000000000000, -1.500000000000000000 ) ) ;
#18836=ORIENTED_EDGE ( 'NONE', *, *, #9705, .F. ) ;
#18843=DIRECTION ( 'NONE',  ( 0.8298699724180969017, -0.5579568342432840167, 0.000000000000000000 ) ) ;
#18861=LINE ( 'NONE', #22531, #944 ) ;
#18862=CARTESIAN_POINT ( 'NONE',  ( 17.25000000000000000, 15.50000000000000178, 7.700000000000001954 ) ) ;
#18869=CIRCLE ( 'NONE', #10294, 1.999999999999997113 ) ;
#18871=FACE_OUTER_BOUND ( 'NONE', #20620, .T. ) ;
#18899=FACE_OUTER_BOUND ( 'NONE', #23356, .T. ) ;
#18911=FACE_OUTER_BOUND ( 'NONE', #15826, .T. ) ;
#18915=AXIS2_PLACEMENT_3D ( 'NONE', #1478, #8890, #16327 ) ;
#18924=CARTESIAN_POINT ( 'NONE',  ( 41.73082370883260239, 27.62204025492843940, -3.000000000000000000 ) ) ;
#18926=DIRECTION ( 'NONE',  ( -0.000000000000000000, -0.000000000000000000, -1.000000000000000000 ) ) ;
#18940=DIRECTION ( 'NONE',  ( -0.000000000000000000, -0.000000000000000000, -1.000000000000000000 ) ) ;
#18946=AXIS2_PLACEMENT_3D ( 'NONE', #14714, #12639, #20107 ) ;
#18964=ORIENTED_EDGE ( 'NONE', *, *, #13807, .T. ) ;
#18965=FACE_OUTER_BOUND ( 'NONE', #7833, .T. ) ;
#18966=AXIS2_PLACEMENT_3D ( 'NONE', #16025, #23490, #8831 ) ;
#18970=CARTESIAN_POINT ( 'NONE',  ( 40.66734255040736201, -26.56420859267091217, -3.000000000000000000 ) ) ;
#18971=CIRCLE ( 'NONE', #1004, 1.500000000000001332 ) ;
#18983=ORIENTED_EDGE ( 'NONE', *, *, #22382, .F. ) ;
#18999=EDGE_CURVE ( 'NONE', #13326, #4606, #20720, .T. ) ;
#19002=CARTESIAN_POINT ( 'NONE',  ( -30.32370777929699202, 42.16181938034195298, 0.000000000000000000 ) ) ;
#19008=VERTEX_POINT ( 'NONE', #22326 ) ;
#19011=AXIS2_PLACEMENT_3D ( 'NONE', #778, #4446, #8070 ) ;
#19012=VERTEX_POINT ( 'NONE', #9609 ) ;
#19027=FACE_OUTER_BOUND ( 'NONE', #12303, .T. ) ;
#19034=ORIENTED_EDGE ( 'NONE', *, *, #13263, .T. ) ;
#19035=CIRCLE ( 'NONE', #17060, 4.249999999999996447 ) ;
#19036=DIRECTION ( 'NONE',  ( -0.000000000000000000, -0.000000000000000000, -1.000000000000000000 ) ) ;
#19039=VERTEX_POINT ( 'NONE', #4879 ) ;
#19055=EDGE_LOOP ( 'NONE', ( #2039, #1169, #9690, #680 ) ) ;
#19058=CARTESIAN_POINT ( 'NONE',  ( 43.50000000000000711, 25.84341543330623026, 0.000000000000000000 ) ) ;
#19061=DIRECTION ( 'NONE',  ( -1.000000000000000000, 0.000000000000000000, 0.000000000000000000 ) ) ;
#19064=CARTESIAN_POINT ( 'NONE',  ( -35.99999999999994316, -60.00000000000000000, 12.50000000000000000 ) ) ;
#19076=ADVANCED_FACE ( 'NONE', ( #15845 ), #14013, .F. ) ;
#19078=ORIENTED_EDGE ( 'NONE', *, *, #19468, .T. ) ;
#19090=VERTEX_POINT ( 'NONE', #12295 ) ;
#19100=CARTESIAN_POINT ( 'NONE',  ( 40.23082370883257397, -29.49999999999999645, -1.500000000000000000 ) ) ;
#19124=ORIENTED_EDGE ( 'NONE', *, *, #22971, .T. ) ;
#19126=DIRECTION ( 'NONE',  ( -0.000000000000000000, -0.000000000000000000, -1.000000000000000000 ) ) ;
#19138=DIRECTION ( 'NONE',  ( 1.000000000000000000, 0.000000000000000000, 0.000000000000000000 ) ) ;
#19145=EDGE_LOOP ( 'NONE', ( #4218, #10805, #2816, #16724, #17781, #18475, #15528, #17020 ) ) ;
#19150=CARTESIAN_POINT ( 'NONE',  ( -1.029124893018731811E-15, 45.00000000000000000, 1.201721238055119212 ) ) ;
#19158=LINE ( 'NONE', #8151, #1311 ) ;
#19161=CIRCLE ( 'NONE', #8627, 11.23082370883260772 ) ;
#19172=CARTESIAN_POINT ( 'NONE',  ( -40.23082370883257397, -29.50000000000000711, -3.000000000000000000 ) ) ;
#19184=EDGE_CURVE ( 'NONE', #12205, #8729, #14465, .T. ) ;
#19185=EDGE_CURVE ( 'NONE', #17955, #1921, #2820, .T. ) ;
#19194=ORIENTED_EDGE ( 'NONE', *, *, #3350, .F. ) ;
#19195=LINE ( 'NONE', #664, #23320 ) ;
#19196=AXIS2_PLACEMENT_3D ( 'NONE', #5764, #3557, #3454 ) ;
#19198=ORIENTED_EDGE ( 'NONE', *, *, #4677, .T. ) ;
#19201=DIRECTION ( 'NONE',  ( 0.000000000000000000, -0.000000000000000000, -1.000000000000000000 ) ) ;
#19217=EDGE_CURVE ( 'NONE', #910, #17727, #2025, .T. ) ;
#19225=DIRECTION ( 'NONE',  ( 0.9945797436152715720, 0.1039766011667100365, -0.000000000000000000 ) ) ;
#19227=DIRECTION ( 'NONE',  ( -1.000000000000000000, 0.000000000000000000, 0.000000000000000000 ) ) ;
#19228=CARTESIAN_POINT ( 'NONE',  ( 2.024999999999999911, -45.00000000000000000, -3.000000000000000000 ) ) ;
#19232=DIRECTION ( 'NONE',  ( 0.000000000000000000, 1.000000000000000000, 0.000000000000000000 ) ) ;
#19237=CYLINDRICAL_SURFACE ( 'NONE', #1558, 40.00000000000000000 ) ;
#19239=AXIS2_PLACEMENT_3D ( 'NONE', #5792, #11136, #1893 ) ;
#19272=CARTESIAN_POINT ( 'NONE',  ( -45.00000000000000000, -50.99999999999993605, 12.50000000000000000 ) ) ;
#19274=ORIENTED_EDGE ( 'NONE', *, *, #12812, .T. ) ;
#19280=CIRCLE ( 'NONE', #14592, 2.024999999999999911 ) ;
#19281=ORIENTED_EDGE ( 'NONE', *, *, #20956, .T. ) ;
#19293=ORIENTED_EDGE ( 'NONE', *, *, #3538, .F. ) ;
#19294=DIRECTION ( 'NONE',  ( -0.000000000000000000, -0.000000000000000000, 1.000000000000000000 ) ) ;
#19300=EDGE_CURVE ( 'NONE', #21933, #16608, #18032, .T. ) ;
#19313=DIRECTION ( 'NONE',  ( -1.000000000000000000, 0.000000000000000000, 0.000000000000000000 ) ) ;
#19338=LINE ( 'NONE', #22989, #19653 ) ;
#19341=DIRECTION ( 'NONE',  ( -0.7089874389501492624, 0.7052211081716913688, 0.000000000000000000 ) ) ;
#19346=CIRCLE ( 'NONE', #15414, 1.499999999999994449 ) ;
#19347=VECTOR ( 'NONE', #3080, 1000.000000000000000 ) ;
#19353=ORIENTED_EDGE ( 'NONE', *, *, #11055, .F. ) ;
#19354=CARTESIAN_POINT ( 'NONE',  ( 23.97500000000000497, -29.50000000000000000, -3.000000000000000000 ) ) ;
#19364=ORIENTED_EDGE ( 'NONE', *, *, #2343, .F. ) ;
#19365=CIRCLE ( 'NONE', #15835, 1.999999999999996669 ) ;
#19386=DIRECTION ( 'NONE',  ( 1.000000000000000000, 0.000000000000000000, 0.000000000000000000 ) ) ;
#19414=FACE_BOUND ( 'NONE', #18400, .T. ) ;
#19422=CARTESIAN_POINT ( 'NONE',  ( 40.23082370883257397, -27.62204025492844650, -3.000000000000000000 ) ) ;
#19425=CARTESIAN_POINT ( 'NONE',  ( -41.73082370883260239, 50.99999999999999289, 0.000000000000000000 ) ) ;
#19429=VERTEX_POINT ( 'NONE', #7745 ) ;
#19430=CARTESIAN_POINT ( 'NONE',  ( 29.00000000000000000, 29.50000000000000000, 14.00000000000000178 ) ) ;
#19438=ORIENTED_EDGE ( 'NONE', *, *, #14103, .T. ) ;
#19444=DIRECTION ( 'NONE',  ( 0.000000000000000000, 0.000000000000000000, 1.000000000000000000 ) ) ;
#19446=CARTESIAN_POINT ( 'NONE',  ( -40.23082370883257397, -29.50000000000000711, -3.000000000000000000 ) ) ;
#19451=CARTESIAN_POINT ( 'NONE',  ( -40.23082370883260239, 27.62204025492846071, -3.000000000000000000 ) ) ;
#19453=CARTESIAN_POINT ( 'NONE',  ( -44.00000000000000711, -51.00000000000000711, 0.5000000000000000000 ) ) ;
#19454=CARTESIAN_POINT ( 'NONE',  ( -45.00000000000001421, 50.99999999999992184, 12.50000000000000000 ) ) ;
#19468=EDGE_CURVE ( 'NONE', #6547, #15558, #7372, .T. ) ;
#19477=DIRECTION ( 'NONE',  ( 0.7089874389501492624, 0.7052211081716913688, 0.000000000000000000 ) ) ;
#19478=DIRECTION ( 'NONE',  ( 0.000000000000000000, -1.000000000000000000, 0.000000000000000000 ) ) ;
#19480=CARTESIAN_POINT ( 'NONE',  ( 35.99999999999999289, 50.99999999999999289, 0.5000000000000004441 ) ) ;
#19491=VERTEX_POINT ( 'NONE', #4848 ) ;
#19506=CARTESIAN_POINT ( 'NONE',  ( 35.99999999999999289, 50.99999999999999289, 0.000000000000000000 ) ) ;
#19540=EDGE_CURVE ( 'NONE', #5523, #12511, #19602, .T. ) ;
#19541=DIRECTION ( 'NONE',  ( 1.000000000000000000, 0.000000000000000000, 0.000000000000000000 ) ) ;
#19546=EDGE_CURVE ( 'NONE', #5954, #1470, #12010, .T. ) ;
#19552=ADVANCED_FACE ( 'NONE', ( #17630 ), #19237, .T. ) ;
#19561=FACE_OUTER_BOUND ( 'NONE', #7450, .T. ) ;
#19565=VECTOR ( 'NONE', #8022, 999.9999999999998863 ) ;
#19571=LINE ( 'NONE', #1153, #9469 ) ;
#19572=AXIS2_PLACEMENT_3D ( 'NONE', #2322, #22695, #5984 ) ;
#19573=CARTESIAN_POINT ( 'NONE',  ( -40.23082370883260239, 27.62204025492846071, -1.500000000000000000 ) ) ;
#19574=DIRECTION ( 'NONE',  ( 0.7052211081716914798, 0.7089874389501492624, -0.000000000000000000 ) ) ;
#19578=CARTESIAN_POINT ( 'NONE',  ( -28.99999999999999645, 29.50000000000000711, -1.500000000000000000 ) ) ;
#19580=CARTESIAN_POINT ( 'NONE',  ( -28.99999999999999645, 29.50000000000000000, 14.00000000000000178 ) ) ;
#19584=ORIENTED_EDGE ( 'NONE', *, *, #19300, .T. ) ;
#19594=ORIENTED_EDGE ( 'NONE', *, *, #4917, .T. ) ;
#19602=LINE ( 'NONE', #6665, #15158 ) ;
#19606=VECTOR ( 'NONE', #11036, 1000.000000000000000 ) ;
#19607=CYLINDRICAL_SURFACE ( 'NONE', #3264, 15.00000000000000000 ) ;
#19616=DIRECTION ( 'NONE',  ( -1.000000000000000000, 0.000000000000000000, 0.000000000000000000 ) ) ;
#19628=DIRECTION ( 'NONE',  ( 0.000000000000000000, -0.000000000000000000, 1.000000000000000000 ) ) ;
#19630=DIRECTION ( 'NONE',  ( -0.000000000000000000, -0.000000000000000000, -1.000000000000000000 ) ) ;
#19631=AXIS2_PLACEMENT_3D ( 'NONE', #11927, #13646, #19138 ) ;
#19653=VECTOR ( 'NONE', #4691, 1000.000000000000000 ) ;
#19658=CARTESIAN_POINT ( 'NONE',  ( 41.73082370883258108, -29.49999999999999645, 0.000000000000000000 ) ) ;
#19662=CARTESIAN_POINT ( 'NONE',  ( 40.23082370883258818, -29.49999999999999645, -1.500000000000000000 ) ) ;
#19668=DIRECTION ( 'NONE',  ( -1.000000000000000000, 0.000000000000000000, 0.000000000000000000 ) ) ;
#19689=ORIENTED_EDGE ( 'NONE', *, *, #22569, .F. ) ;
#19691=EDGE_CURVE ( 'NONE', #12610, #15653, #18136, .T. ) ;
#19695=EDGE_CURVE ( 'NONE', #10068, #2874, #1166, .T. ) ;
#19706=CARTESIAN_POINT ( 'NONE',  ( -35.99999999999994316, -60.00000000000000000, 0.000000000000000000 ) ) ;
#19709=CYLINDRICAL_SURFACE ( 'NONE', #22379, 4.249999999999996447 ) ;
#19712=AXIS2_PLACEMENT_3D ( 'NONE', #11713, #9895, #17353 ) ;
#19715=AXIS2_PLACEMENT_3D ( 'NONE', #738, #21359, #2683 ) ;
#19716=AXIS2_PLACEMENT_3D ( 'NONE', #11072, #19036, #20867 ) ;
#19718=DIRECTION ( 'NONE',  ( 0.7071067811865474617, 8.659560562354932858E-17, -0.7071067811865474617 ) ) ;
#19729=FACE_OUTER_BOUND ( 'NONE', #3140, .T. ) ;
#19742=ORIENTED_EDGE ( 'NONE', *, *, #14383, .T. ) ;
#19756=CARTESIAN_POINT ( 'NONE',  ( 40.23082370883260239, 29.49999999999999645, -3.000000000000000000 ) ) ;
#19761=CARTESIAN_POINT ( 'NONE',  ( 24.75000000000000711, -29.50000000000000000, -2.224999999999995204 ) ) ;
#19769=FACE_OUTER_BOUND ( 'NONE', #6286, .T. ) ;
#19781=CARTESIAN_POINT ( 'NONE',  ( 35.99999999999999289, -51.00000000000000711, 0.5000000000000004441 ) ) ;
#19786=DIRECTION ( 'NONE',  ( -0.000000000000000000, -0.000000000000000000, -1.000000000000000000 ) ) ;
#19788=EDGE_CURVE ( 'NONE', #5633, #1485, #21239, .T. ) ;
#19806=EDGE_CURVE ( 'NONE', #747, #1952, #2086, .T. ) ;
#19809=ADVANCED_FACE ( 'NONE', ( #22704, #15374 ), #11697, .T. ) ;
#19816=ORIENTED_EDGE ( 'NONE', *, *, #15421, .F. ) ;
#19822=CARTESIAN_POINT ( 'NONE',  ( 43.99999999999999289, -51.00000000000000711, 0.5000000000000000000 ) ) ;
#19829=CIRCLE ( 'NONE', #12402, 49.99999999999998579 ) ;
#19838=EDGE_LOOP ( 'NONE', ( #10064, #34 ) ) ;
#19841=CARTESIAN_POINT ( 'NONE',  ( 41.73082370883260239, 27.62204025492843940, -1.500000000000000000 ) ) ;
#19852=ORIENTED_EDGE ( 'NONE', *, *, #2010, .F. ) ;
#19864=DIRECTION ( 'NONE',  ( 0.000000000000000000, 0.000000000000000000, 1.000000000000000000 ) ) ;
#19866=CARTESIAN_POINT ( 'NONE',  ( 41.73082370883257397, -27.62204025492843940, -1.500000000000000000 ) ) ;
#19873=CARTESIAN_POINT ( 'NONE',  ( -1.999999999999996669, -45.00000000000000000, -8.673617379884035472E-16 ) ) ;
#19874=ORIENTED_EDGE ( 'NONE', *, *, #9392, .T. ) ;
#19889=DIRECTION ( 'NONE',  ( -1.000000000000000000, 0.000000000000000000, 0.000000000000000000 ) ) ;
#19906=ORIENTED_EDGE ( 'NONE', *, *, #14141, .T. ) ;
#19908=EDGE_CURVE ( 'NONE', #2673, #6921, #13631, .T. ) ;
#19909=CARTESIAN_POINT ( 'NONE',  ( 0.000000000000000000, -45.00000000000000000, -2.974999999999996092 ) ) ;
#19910=EDGE_CURVE ( 'NONE', #17944, #16608, #9724, .T. ) ;
#19912=CARTESIAN_POINT ( 'NONE',  ( 41.99999999999997158, -25.22443390181681622, -1.500000000000000000 ) ) ;
#19926=DIRECTION ( 'NONE',  ( -0.000000000000000000, -0.000000000000000000, -1.000000000000000000 ) ) ;
#19930=CARTESIAN_POINT ( 'NONE',  ( -30.68762588338048403, 45.64284848299540442, -3.000000000000000000 ) ) ;
#19944=CARTESIAN_POINT ( 'NONE',  ( 28.73477696352899713, 42.73830357953205095, 0.000000000000000000 ) ) ;
#19947=CARTESIAN_POINT ( 'NONE',  ( 33.24999999999999289, 29.50000000000000000, 14.00000000000000178 ) ) ;
#19960=ORIENTED_EDGE ( 'NONE', *, *, #7304, .T. ) ;
#19964=AXIS2_PLACEMENT_3D ( 'NONE', #3794, #17185, #2070 ) ;
#19967=CIRCLE ( 'NONE', #17616, 4.249999999999993783 ) ;
#19971=CIRCLE ( 'NONE', #13329, 5.000000000000000888 ) ;
#19977=DIRECTION ( 'NONE',  ( -1.000000000000000000, 0.000000000000000000, 0.000000000000000000 ) ) ;
#19987=FACE_OUTER_BOUND ( 'NONE', #11252, .T. ) ;
#19992=EDGE_LOOP ( 'NONE', ( #17582, #23820, #4055, #9847 ) ) ;
#20003=DIRECTION ( 'NONE',  ( -0.000000000000000000, -0.000000000000000000, 1.000000000000000000 ) ) ;
#20012=DIRECTION ( 'NONE',  ( -0.000000000000000000, -0.000000000000000000, -1.000000000000000000 ) ) ;
#20026=AXIS2_PLACEMENT_3D ( 'NONE', #673, #15526, #17603 ) ;
#20043=EDGE_CURVE ( 'NONE', #2834, #13441, #1943, .T. ) ;
#20063=CIRCLE ( 'NONE', #4484, 10.00000000000000533 ) ;
#20065=ORIENTED_EDGE ( 'NONE', *, *, #14116, .F. ) ;
#20080=CYLINDRICAL_SURFACE ( 'NONE', #17267, 8.000000000000000000 ) ;
#20086=CONICAL_SURFACE ( 'NONE', #4093, 5.024999999999998579, 0.7853981633974438381 ) ;
#20090=CONICAL_SURFACE ( 'NONE', #271, 1.999999999999996669, 1.029744258676653867 ) ;
#20094=CARTESIAN_POINT ( 'NONE',  ( 29.00000000000000000, 29.50000000000000000, -3.000000000000000000 ) ) ;
#20096=ORIENTED_EDGE ( 'NONE', *, *, #16676, .F. ) ;
#20097=EDGE_CURVE ( 'NONE', #21933, #15211, #10893, .T. ) ;
#20107=DIRECTION ( 'NONE',  ( -1.000000000000000000, 0.000000000000000000, 0.000000000000000000 ) ) ;
#20114=CARTESIAN_POINT ( 'NONE',  ( -36.00000000000000711, -51.00000000000000711, 0.5000000000000000000 ) ) ;
#20115=DIRECTION ( 'NONE',  ( 0.000000000000000000, 0.000000000000000000, -1.000000000000000000 ) ) ;
#20126=ORIENTED_EDGE ( 'NONE', *, *, #20724, .T. ) ;
#20133=LINE ( 'NONE', #8633, #9767 ) ;
#20135=ADVANCED_FACE ( 'NONE', ( #22213 ), #3304, .F. ) ;
#20145=CIRCLE ( 'NONE', #18966, 1.999999999999997113 ) ;
#20151=DIRECTION ( 'NONE',  ( -1.000000000000000000, 0.000000000000000000, 0.000000000000000000 ) ) ;
#20153=ORIENTED_EDGE ( 'NONE', *, *, #3538, .T. ) ;
#20164=EDGE_CURVE ( 'NONE', #3028, #5633, #18552, .T. ) ;
#20165=CARTESIAN_POINT ( 'NONE',  ( 0.000000000000000000, 15.50000000000000000, 16.70000000000000284 ) ) ;
#20177=CARTESIAN_POINT ( 'NONE',  ( 30.16774287754691386, -40.66994976491903913, -1.500000000000000000 ) ) ;
#20180=LINE ( 'NONE', #14189, #20744 ) ;
#20183=DIRECTION ( 'NONE',  ( -1.000000000000000000, 0.000000000000000000, 0.000000000000000000 ) ) ;
#20186=CIRCLE ( 'NONE', #20965, 8.000000000000000000 ) ;
#20205=DIRECTION ( 'NONE',  ( -0.000000000000000000, -0.000000000000000000, 1.000000000000000000 ) ) ;
#20207=CARTESIAN_POINT ( 'NONE',  ( 27.89784171216407316, -41.49349862090490149, -1.500000000000000000 ) ) ;
#20235=CARTESIAN_POINT ( 'NONE',  ( 3.890962118697714531E-15, 15.50000000000000000, 19.70000000000000284 ) ) ;
#20236=VERTEX_POINT ( 'NONE', #19272 ) ;
#20242=EDGE_LOOP ( 'NONE', ( #52, #20707, #20275, #7967 ) ) ;
#20243=EDGE_CURVE ( 'NONE', #1485, #19491, #125, .T. ) ;
#20262=ORIENTED_EDGE ( 'NONE', *, *, #15829, .F. ) ;
#20264=ORIENTED_EDGE ( 'NONE', *, *, #15232, .T. ) ;
#20269=CARTESIAN_POINT ( 'NONE',  ( 43.49999999999997868, -25.84341543330623381, 0.000000000000000000 ) ) ;
#20273=DIRECTION ( 'NONE',  ( -1.000000000000000000, 0.000000000000000000, 0.000000000000000000 ) ) ;
#20275=ORIENTED_EDGE ( 'NONE', *, *, #24079, .T. ) ;
#20277=LINE ( 'NONE', #16485, #4874 ) ;
#20281=CARTESIAN_POINT ( 'NONE',  ( 35.99999999999999289, 50.99999999999999289, 12.50000000000000000 ) ) ;
#20294=ORIENTED_EDGE ( 'NONE', *, *, #16916, .F. ) ;
#20296=EDGE_LOOP ( 'NONE', ( #5863, #14881, #3789, #15982 ) ) ;
#20299=ORIENTED_EDGE ( 'NONE', *, *, #15159, .F. ) ;
#20302=DIRECTION ( 'NONE',  ( -0.000000000000000000, -0.000000000000000000, -1.000000000000000000 ) ) ;
#20310=FACE_BOUND ( 'NONE', #4808, .T. ) ;
#20318=VERTEX_POINT ( 'NONE', #13535 ) ;
#20322=ORIENTED_EDGE ( 'NONE', *, *, #23513, .F. ) ;
#20324=CARTESIAN_POINT ( 'NONE',  ( -30.32370777929697425, -42.16181938034195298, -1.500000000000000000 ) ) ;
#20340=DIRECTION ( 'NONE',  ( 0.7052211081716891483, 0.7089874389501515939, -0.000000000000000000 ) ) ;
#20344=LINE ( 'NONE', #3151, #11374 ) ;
#20356=AXIS2_PLACEMENT_3D ( 'NONE', #4142, #11557, #11665 ) ;
#20357=CARTESIAN_POINT ( 'NONE',  ( 28.99999999999998579, -29.49999999999999645, -1.500000000000000000 ) ) ;
#20358=AXIS2_PLACEMENT_3D ( 'NONE', #9390, #15247, #15019 ) ;
#20365=ADVANCED_FACE ( 'NONE', ( #19769 ), #21349, .T. ) ;
#20371=DIRECTION ( 'NONE',  ( 0.000000000000000000, 0.000000000000000000, 1.000000000000000000 ) ) ;
#20372=DIRECTION ( 'NONE',  ( 5.501724186093585079E-16, 1.000000000000000000, -0.000000000000000000 ) ) ;
#20382=DIRECTION ( 'NONE',  ( 1.000000000000000000, 0.000000000000000000, 0.000000000000000000 ) ) ;
#20384=CARTESIAN_POINT ( 'NONE',  ( -41.73082370883260239, 29.50000000000000711, -1.500000000000000000 ) ) ;
#20385=EDGE_CURVE ( 'NONE', #4271, #21210, #16517, .T. ) ;
#20407=ORIENTED_EDGE ( 'NONE', *, *, #17919, .F. ) ;
#20409=ORIENTED_EDGE ( 'NONE', *, *, #13246, .T. ) ;
#20413=VECTOR ( 'NONE', #6398, 999.9999999999998863 ) ;
#20417=CYLINDRICAL_SURFACE ( 'NONE', #136, 10.00000000000000178 ) ;
#20418=ORIENTED_EDGE ( 'NONE', *, *, #4550, .F. ) ;
#20423=ORIENTED_EDGE ( 'NONE', *, *, #21862, .F. ) ;
#20424=DIRECTION ( 'NONE',  ( -0.000000000000000000, -0.000000000000000000, -1.000000000000000000 ) ) ;
#20425=FACE_OUTER_BOUND ( 'NONE', #2210, .T. ) ;
#20427=FACE_OUTER_BOUND ( 'NONE', #6038, .T. ) ;
#20438=AXIS2_PLACEMENT_3D ( 'NONE', #1807, #16555, #5580 ) ;
#20449=PLANE ( 'NONE',  #9468 ) ;
#20460=ORIENTED_EDGE ( 'NONE', *, *, #1700, .F. ) ;
#20462=ORIENTED_EDGE ( 'NONE', *, *, #247, .T. ) ;
#20477=VECTOR ( 'NONE', #7941, 1000.000000000000000 ) ;
#20497=CIRCLE ( 'NONE', #13076, 11.23082370883260772 ) ;
#20502=CONICAL_SURFACE ( 'NONE', #17376, 1.999999999999996669, 1.029744258676653867 ) ;
#20505=ORIENTED_EDGE ( 'NONE', *, *, #10015, .T. ) ;
#20506=EDGE_CURVE ( 'NONE', #16565, #10152, #1099, .T. ) ;
#20508=VERTEX_POINT ( 'NONE', #8519 ) ;
#20513=DIRECTION ( 'NONE',  ( -0.000000000000000000, -0.000000000000000000, -1.000000000000000000 ) ) ;
#20515=EDGE_CURVE ( 'NONE', #8450, #5111, #6002, .T. ) ;
#20517=ADVANCED_FACE ( 'NONE', ( #22190 ), #5627, .F. ) ;
#20518=CIRCLE ( 'NONE', #18946, 1.999999999999996669 ) ;
#20522=LINE ( 'NONE', #22474, #9820 ) ;
#20527=FACE_OUTER_BOUND ( 'NONE', #10134, .T. ) ;
#20532=ORIENTED_EDGE ( 'NONE', *, *, #9021, .T. ) ;
#20547=EDGE_CURVE ( 'NONE', #779, #13326, #14604, .T. ) ;
#20565=CARTESIAN_POINT ( 'NONE',  ( -30.16774287754690675, -40.66994976491903913, -3.000000000000000000 ) ) ;
#20569=ORIENTED_EDGE ( 'NONE', *, *, #23762, .F. ) ;
#20589=DIRECTION ( 'NONE',  ( 1.000000000000000000, 0.000000000000000000, 0.000000000000000000 ) ) ;
#20593=LINE ( 'NONE', #15447, #7413 ) ;
#20598=ORIENTED_EDGE ( 'NONE', *, *, #14454, .F. ) ;
#20601=VERTEX_POINT ( 'NONE', #22299 ) ;
#20605=DIRECTION ( 'NONE',  ( -0.000000000000000000, -0.000000000000000000, -1.000000000000000000 ) ) ;
#20615=EDGE_CURVE ( 'NONE', #13428, #20777, #9513, .T. ) ;
#20620=EDGE_LOOP ( 'NONE', ( #16872, #16736, #1049, #8478 ) ) ;
#20622=ORIENTED_EDGE ( 'NONE', *, *, #2579, .F. ) ;
#20626=CARTESIAN_POINT ( 'NONE',  ( 33.25000000000000000, 29.50000000000000000, -2.224999999999995204 ) ) ;
#20634=CARTESIAN_POINT ( 'NONE',  ( 0.000000000000000000, 0.000000000000000000, 0.000000000000000000 ) ) ;
#20637=EDGE_CURVE ( 'NONE', #16656, #15558, #10573, .T. ) ;
#20642=CARTESIAN_POINT ( 'NONE',  ( 17.25000000000000000, 15.50000000000000178, 14.70000000000000284 ) ) ;
#20667=FACE_BOUND ( 'NONE', #5810, .T. ) ;
#20669=DIRECTION ( 'NONE',  ( 0.7071067811865574537, 8.659560562355054885E-17, -0.7071067811865376918 ) ) ;
#20671=ORIENTED_EDGE ( 'NONE', *, *, #14219, .F. ) ;
#20674=ORIENTED_EDGE ( 'NONE', *, *, #3577, .F. ) ;
#20680=ORIENTED_EDGE ( 'NONE', *, *, #20547, .T. ) ;
#20702=EDGE_LOOP ( 'NONE', ( #8332, #2897, #23314, #8155 ) ) ;
#20704=VECTOR ( 'NONE', #10475, 1000.000000000000114 ) ;
#20707=ORIENTED_EDGE ( 'NONE', *, *, #11661, .T. ) ;
#20711=CARTESIAN_POINT ( 'NONE',  ( -27.89784171216405895, -41.49349862090491570, -3.000000000000000000 ) ) ;
#20720=CIRCLE ( 'NONE', #3961, 1.999999999999996669 ) ;
#20724=EDGE_CURVE ( 'NONE', #20777, #13428, #5245, .T. ) ;
#20744=VECTOR ( 'NONE', #10871, 1000.000000000000000 ) ;
#20754=VECTOR ( 'NONE', #833, 1000.000000000000000 ) ;
#20759=CYLINDRICAL_SURFACE ( 'NONE', #14142, 4.499999999999997335 ) ;
#20765=VECTOR ( 'NONE', #278, 1000.000000000000000 ) ;
#20769=VECTOR ( 'NONE', #15425, 1000.000000000000000 ) ;
#20772=EDGE_LOOP ( 'NONE', ( #4411, #3945, #17868, #11513 ) ) ;
#20777=VERTEX_POINT ( 'NONE', #13898 ) ;
#20785=ORIENTED_EDGE ( 'NONE', *, *, #11055, .T. ) ;
#20792=DIRECTION ( 'NONE',  ( -0.7052211081716895924, -0.7089874389501510388, -0.000000000000000000 ) ) ;
#20793=DIRECTION ( 'NONE',  ( 1.000000000000000000, 0.000000000000000000, 0.000000000000000000 ) ) ;
#20797=CYLINDRICAL_SURFACE ( 'NONE', #12986, 4.499999999999997335 ) ;
#20799=ORIENTED_EDGE ( 'NONE', *, *, #15610, .T. ) ;
#20803=EDGE_CURVE ( 'NONE', #17488, #18602, #4074, .T. ) ;
#20808=AXIS2_PLACEMENT_3D ( 'NONE', #17021, #11887, #15167 ) ;
#20811=VECTOR ( 'NONE', #17542, 1000.000000000000000 ) ;
#20818=EDGE_CURVE ( 'NONE', #1952, #13312, #23999, .T. ) ;
#20824=DIRECTION ( 'NONE',  ( 0.7052211081716905916, 0.7089874389501501506, 0.000000000000000000 ) ) ;
#20834=LINE ( 'NONE', #17032, #17268 ) ;
#20840=VERTEX_POINT ( 'NONE', #18509 ) ;
#20846=AXIS2_PLACEMENT_3D ( 'NONE', #6598, #23327, #13661 ) ;
#20848=EDGE_LOOP ( 'NONE', ( #18044, #8028 ) ) ;
#20854=DIRECTION ( 'NONE',  ( -5.501724186093585079E-16, -1.000000000000000000, 0.000000000000000000 ) ) ;
#20858=CIRCLE ( 'NONE', #11081, 8.999999999999994671 ) ;
#20861=DIRECTION ( 'NONE',  ( -0.000000000000000000, -0.000000000000000000, -1.000000000000000000 ) ) ;
#20867=DIRECTION ( 'NONE',  ( -1.000000000000000000, 0.000000000000000000, 0.000000000000000000 ) ) ;
#20889=CYLINDRICAL_SURFACE ( 'NONE', #7504, 15.00000000000000000 ) ;
#20892=CARTESIAN_POINT ( 'NONE',  ( 42.62132034355964549, 25.48082444701819682, 9.418351429901832011E-16 ) ) ;
#20905=VECTOR ( 'NONE', #4707, 1000.000000000000000 ) ;
#20914=CARTESIAN_POINT ( 'NONE',  ( -28.99999999999999645, -29.50000000000000000, -2.224999999999995204 ) ) ;
#20925=CARTESIAN_POINT ( 'NONE',  ( 24.75000000000000711, 29.50000000000000000, 14.00000000000000178 ) ) ;
#20927=LINE ( 'NONE', #19454, #21185 ) ;
#20931=CIRCLE ( 'NONE', #11550, 1.500000000000001332 ) ;
#20947=CARTESIAN_POINT ( 'NONE',  ( -28.99999999999999645, 29.50000000000000000, -3.000000000000000000 ) ) ;
#20955=CARTESIAN_POINT ( 'NONE',  ( 40.23082370883260239, 29.49999999999999645, -1.500000000000000000 ) ) ;
#20956=EDGE_CURVE ( 'NONE', #4606, #13326, #17726, .T. ) ;
#20962=DIRECTION ( 'NONE',  ( -0.000000000000000000, -0.000000000000000000, -1.000000000000000000 ) ) ;
#20965=AXIS2_PLACEMENT_3D ( 'NONE', #14715, #22533, #12762 ) ;
#20972=CARTESIAN_POINT ( 'NONE',  ( 27.19186005726088240, 42.23865125093339401, 0.000000000000000000 ) ) ;
#20975=DIRECTION ( 'NONE',  ( 1.000000000000000000, 0.000000000000000000, 0.000000000000000000 ) ) ;
#20979=EDGE_CURVE ( 'NONE', #13946, #978, #7061, .T. ) ;
#20989=CARTESIAN_POINT ( 'NONE',  ( 0.000000000000000000, 0.000000000000000000, -1.500000000000000000 ) ) ;
#21012=CARTESIAN_POINT ( 'NONE',  ( 35.99999999999999289, 50.99999999999999289, 0.5000000000000000000 ) ) ;
#21015=EDGE_LOOP ( 'NONE', ( #13511, #19353, #2459, #17459 ) ) ;
#21028=EDGE_CURVE ( 'NONE', #2131, #16878, #11460, .T. ) ;
#21031=PLANE ( 'NONE',  #10976 ) ;
#21049=CARTESIAN_POINT ( 'NONE',  ( -28.99999999999999645, 29.50000000000000000, 14.00000000000000178 ) ) ;
#21054=DIRECTION ( 'NONE',  ( -0.000000000000000000, -0.000000000000000000, -1.000000000000000000 ) ) ;
#21069=VERTEX_POINT ( 'NONE', #14748 ) ;
#21075=EDGE_CURVE ( 'NONE', #5633, #2260, #13529, .T. ) ;
#21086=EDGE_LOOP ( 'NONE', ( #9947, #6297, #10493 ) ) ;
#21088=EDGE_LOOP ( 'NONE', ( #22629, #17437, #22380, #20622 ) ) ;
#21092=VERTEX_POINT ( 'NONE', #15337 ) ;
#21094=ADVANCED_FACE ( 'NONE', ( #19027 ), #20086, .F. ) ;
#21103=AXIS2_PLACEMENT_3D ( 'NONE', #21870, #12576, #1854 ) ;
#21113=DIRECTION ( 'NONE',  ( -5.501724186093582121E-16, 1.000000000000000000, 0.000000000000000000 ) ) ;
#21124=AXIS2_PLACEMENT_3D ( 'NONE', #4011, #7310, #18303 ) ;
#21126=DIRECTION ( 'NONE',  ( -0.000000000000000000, -0.000000000000000000, -1.000000000000000000 ) ) ;
#21128=ORIENTED_EDGE ( 'NONE', *, *, #8497, .T. ) ;
#21158=ORIENTED_EDGE ( 'NONE', *, *, #19546, .F. ) ;
#21159=ADVANCED_FACE ( 'NONE', ( #22558 ), #16947, .T. ) ;
#21168=LINE ( 'NONE', #19354, #1291 ) ;
#21171=AXIS2_PLACEMENT_3D ( 'NONE', #22124, #5393, #20273 ) ;
#21183=CYLINDRICAL_SURFACE ( 'NONE', #12504, 8.000000000000000000 ) ;
#21185=VECTOR ( 'NONE', #11620, 1000.000000000000000 ) ;
#21186=CIRCLE ( 'NONE', #9859, 15.00000000000000000 ) ;
#21187=CIRCLE ( 'NONE', #2071, 3.500000000000003109 ) ;
#21189=AXIS2_PLACEMENT_3D ( 'NONE', #7827, #2360, #16652 ) ;
#21194=ORIENTED_EDGE ( 'NONE', *, *, #18309, .F. ) ;
#21200=CARTESIAN_POINT ( 'NONE',  ( 3.890962118697714531E-15, 15.50000000000000000, 7.699999999999998401 ) ) ;
#21210=VERTEX_POINT ( 'NONE', #2180 ) ;
#21213=AXIS2_PLACEMENT_3D ( 'NONE', #16680, #3626, #10918 ) ;
#21225=VERTEX_POINT ( 'NONE', #9607 ) ;
#21239=( BOUNDED_CURVE ( )  B_SPLINE_CURVE ( 3, ( #19058, #20892, #11004, #16967 ),
 .UNSPECIFIED., .F., .T. ) 
 B_SPLINE_CURVE_WITH_KNOTS ( ( 4, 4 ),
 ( 4.712388980384688786, 6.283185307179586232 ),
 .UNSPECIFIED. ) 
 CURVE ( )  GEOMETRIC_REPRESENTATION_ITEM ( )  RATIONAL_B_SPLINE_CURVE ( ( 1.000000000000000000, 0.8047378541243648264, 0.8047378541243648264, 1.000000000000000000 ) ) 
 REPRESENTATION_ITEM ( '' )  );
#21241=ORIENTED_EDGE ( 'NONE', *, *, #13954, .T. ) ;
#21252=DIRECTION ( 'NONE',  ( -1.000000000000000000, 0.000000000000000000, 0.000000000000000000 ) ) ;
#21275=EDGE_LOOP ( 'NONE', ( #19742, #4306, #17375, #15722, #18647, #12767, #4790, #21128, #16934, #14173, #2593, #9188, #22893, #14046, #10563, #1924, #7264, #7104, #11956, #16533 ) ) ;
#21283=DIRECTION ( 'NONE',  ( 0.000000000000000000, -1.000000000000000000, 0.000000000000000000 ) ) ;
#21285=CIRCLE ( 'NONE', #11909, 4.499999999999997335 ) ;
#21286=CARTESIAN_POINT ( 'NONE',  ( -30.16774287754692807, 40.66994976491904623, -3.000000000000000000 ) ) ;
#21288=DIRECTION ( 'NONE',  ( -0.000000000000000000, -0.000000000000000000, -1.000000000000000000 ) ) ;
#21295=ORIENTED_EDGE ( 'NONE', *, *, #20097, .F. ) ;
#21343=DIRECTION ( 'NONE',  ( -1.000000000000000000, 0.000000000000000000, 0.000000000000000000 ) ) ;
#21345=CYLINDRICAL_SURFACE ( 'NONE', #18411, 9.000000000000001776 ) ;
#21348=EDGE_CURVE ( 'NONE', #7111, #15532, #22759, .T. ) ;
#21349=CYLINDRICAL_SURFACE ( 'NONE', #4468, 11.23082370883259706 ) ;
#21356=AXIS2_PLACEMENT_3D ( 'NONE', #8921, #22001, #5283 ) ;
#21359=DIRECTION ( 'NONE',  ( -0.000000000000000000, -0.000000000000000000, -1.000000000000000000 ) ) ;
#21361=DIRECTION ( 'NONE',  ( 0.000000000000000000, -0.000000000000000000, 1.000000000000000000 ) ) ;
#21390=ORIENTED_EDGE ( 'NONE', *, *, #4552, .F. ) ;
#21401=EDGE_LOOP ( 'NONE', ( #15455, #1945, #8043, #14844 ) ) ;
#21422=AXIS2_PLACEMENT_3D ( 'NONE', #6659, #10305, #21426 ) ;
#21423=ADVANCED_FACE ( 'NONE', ( #16127 ), #5296, .F. ) ;
#21425=EDGE_CURVE ( 'NONE', #11173, #23706, #4914, .T. ) ;
#21426=DIRECTION ( 'NONE',  ( 0.000000000000000000, 0.000000000000000000, -1.000000000000000000 ) ) ;
#21429=DIRECTION ( 'NONE',  ( -1.000000000000000000, 0.000000000000000000, 0.000000000000000000 ) ) ;
#21432=CARTESIAN_POINT ( 'NONE',  ( -41.73082370883260239, 27.62204025492845361, -1.500000000000000000 ) ) ;
#21444=EDGE_CURVE ( 'NONE', #4806, #14424, #5676, .T. ) ;
#21445=CARTESIAN_POINT ( 'NONE',  ( 35.99999999999999289, 50.99999999999999289, 12.50000000000000000 ) ) ;
#21450=EDGE_CURVE ( 'NONE', #3540, #6174, #6465, .T. ) ;
#21454=DIRECTION ( 'NONE',  ( 0.8298699724181002324, 0.5579568342432785766, 1.919459897549205054E-15 ) ) ;
#21458=CYLINDRICAL_SURFACE ( 'NONE', #22703, 1.999999999999996669 ) ;
#21462=LINE ( 'NONE', #15959, #19565 ) ;
#21476=PLANE ( 'NONE',  #8803 ) ;
#21487=CARTESIAN_POINT ( 'NONE',  ( 41.99999999999997158, -25.22443390181681622, -3.000000000000000000 ) ) ;
#21490=ORIENTED_EDGE ( 'NONE', *, *, #13851, .F. ) ;
#21494=EDGE_LOOP ( 'NONE', ( #17739, #10408, #3681, #8185 ) ) ;
#21507=CARTESIAN_POINT ( 'NONE',  ( -30.16774287754692807, 40.66994976491904623, -3.000000000000000000 ) ) ;
#21511=DIRECTION ( 'NONE',  ( -1.000000000000000000, 0.000000000000000000, 0.000000000000000000 ) ) ;
#21552=DIRECTION ( 'NONE',  ( -0.000000000000000000, 1.000000000000000000, -0.000000000000000000 ) ) ;
#21554=DIRECTION ( 'NONE',  ( -0.000000000000000000, 1.000000000000000000, -0.000000000000000000 ) ) ;
#21558=CIRCLE ( 'NONE', #12961, 40.00000000000000000 ) ;
#21561=ORIENTED_EDGE ( 'NONE', *, *, #15610, .F. ) ;
#21574=ORIENTED_EDGE ( 'NONE', *, *, #14351, .F. ) ;
#21588=ORIENTED_EDGE ( 'NONE', *, *, #8736, .T. ) ;
#21601=ORIENTED_EDGE ( 'NONE', *, *, #13246, .F. ) ;
#21611=CARTESIAN_POINT ( 'NONE',  ( 1.999999999999996669, 45.00000000000000000, -3.000000000000000000 ) ) ;
#21619=SPHERICAL_SURFACE ( 'NONE', #14623, 1.500000000000000000 ) ;
#21623=ORIENTED_EDGE ( 'NONE', *, *, #9757, .T. ) ;
#21632=AXIS2_PLACEMENT_3D ( 'NONE', #14802, #64, #14918 ) ;
#21634=LINE ( 'NONE', #23708, #9531 ) ;
#21643=AXIS2_PLACEMENT_3D ( 'NONE', #10685, #21454, #1320 ) ;
#21651=ORIENTED_EDGE ( 'NONE', *, *, #13159, .F. ) ;
#21654=DIRECTION ( 'NONE',  ( 1.000000000000000000, 0.000000000000000000, 0.000000000000000000 ) ) ;
#21658=AXIS2_PLACEMENT_3D ( 'NONE', #20165, #5041, #18089 ) ;
#21661=CIRCLE ( 'NONE', #1396, 5.025000000000002132 ) ;
#21665=CARTESIAN_POINT ( 'NONE',  ( 1.999999999999996669, -45.00000000000000000, -8.673617379884035472E-16 ) ) ;
#21669=CIRCLE ( 'NONE', #11110, 11.23082370883259706 ) ;
#21671=ORIENTED_EDGE ( 'NONE', *, *, #8031, .F. ) ;
#21677=CARTESIAN_POINT ( 'NONE',  ( 0.000000000000000000, -45.00000000000000000, -3.000000000000000000 ) ) ;
#21682=CARTESIAN_POINT ( 'NONE',  ( -28.99999999999999645, 29.50000000000000711, -3.000000000000000000 ) ) ;
#21702=ADVANCED_FACE ( 'NONE', ( #22948 ), #15729, .F. ) ;
#21703=DIRECTION ( 'NONE',  ( 0.000000000000000000, 0.000000000000000000, -1.000000000000000000 ) ) ;
#21713=DIRECTION ( 'NONE',  ( 0.000000000000000000, 0.000000000000000000, -1.000000000000000000 ) ) ;
#21731=ORIENTED_EDGE ( 'NONE', *, *, #275, .T. ) ;
#21736=CARTESIAN_POINT ( 'NONE',  ( -31.50000000000000711, -51.00000000000000711, 12.50000000000000000 ) ) ;
#21750=CARTESIAN_POINT ( 'NONE',  ( 43.99999999999999289, -51.00000000000000711, 0.000000000000000000 ) ) ;
#21751=CARTESIAN_POINT ( 'NONE',  ( 40.49999999999998579, 50.99999999999999289, 12.50000000000000000 ) ) ;
#21753=ORIENTED_EDGE ( 'NONE', *, *, #19788, .F. ) ;
#21757=ORIENTED_EDGE ( 'NONE', *, *, #712, .F. ) ;
#21763=EDGE_CURVE ( 'NONE', #5954, #11227, #2966, .T. ) ;
#21765=LINE ( 'NONE', #1513, #18017 ) ;
#21766=AXIS2_PLACEMENT_3D ( 'NONE', #20914, #22738, #15143 ) ;
#21773=CIRCLE ( 'NONE', #1887, 1.499999999999998002 ) ;
#21775=EDGE_LOOP ( 'NONE', ( #542, #1802, #10263, #6289 ) ) ;
#21790=DIRECTION ( 'NONE',  ( -0.000000000000000000, -0.000000000000000000, -1.000000000000000000 ) ) ;
#21792=DIRECTION ( 'NONE',  ( -0.000000000000000000, -0.000000000000000000, -1.000000000000000000 ) ) ;
#21795=CARTESIAN_POINT ( 'NONE',  ( -30.32370777929699202, 42.16181938034195298, -1.500000000000000000 ) ) ;
#21803=VECTOR ( 'NONE', #2513, 1000.000000000000000 ) ;
#21811=ORIENTED_EDGE ( 'NONE', *, *, #12726, .T. ) ;
#21812=CARTESIAN_POINT ( 'NONE',  ( -41.73082370883257397, 50.99999999999999289, 0.000000000000000000 ) ) ;
#21813=VECTOR ( 'NONE', #17892, 1000.000000000000114 ) ;
#21820=DIRECTION ( 'NONE',  ( -0.8571673007021120005, 0.000000000000000000, -0.5150380749100547106 ) ) ;
#21830=ADVANCED_FACE ( 'NONE', ( #6597 ), #21476, .F. ) ;
#21836=CARTESIAN_POINT ( 'NONE',  ( -40.50000000000000711, 50.99999999999999289, 12.50000000000000000 ) ) ;
#21850=EDGE_CURVE ( 'NONE', #7627, #18281, #21285, .T. ) ;
#21855=ORIENTED_EDGE ( 'NONE', *, *, #23042, .F. ) ;
#21862=EDGE_CURVE ( 'NONE', #19012, #5970, #23248, .T. ) ;
#21870=CARTESIAN_POINT ( 'NONE',  ( 41.73082370883260239, 27.62204025492844650, -1.500000000000000000 ) ) ;
#21877=DIRECTION ( 'NONE',  ( -0.000000000000000000, -0.000000000000000000, -1.000000000000000000 ) ) ;
#21887=ORIENTED_EDGE ( 'NONE', *, *, #16121, .T. ) ;
#21894=CIRCLE ( 'NONE', #858, 10.00000000000000178 ) ;
#21904=DIRECTION ( 'NONE',  ( -5.501724186093585079E-16, -1.000000000000000000, 0.000000000000000000 ) ) ;
#21909=VECTOR ( 'NONE', #23789, 1000.000000000000000 ) ;
#21918=ORIENTED_EDGE ( 'NONE', *, *, #15418, .T. ) ;
#21924=PLANE ( 'NONE',  #3710 ) ;
#21925=DIRECTION ( 'NONE',  ( -4.625929269271481378E-15, 1.000000000000000000, 0.000000000000000000 ) ) ;
#21928=AXIS2_PLACEMENT_3D ( 'NONE', #19866, #1204, #23532 ) ;
#21929=AXIS2_PLACEMENT_3D ( 'NONE', #13052, #20513, #22470 ) ;
#21933=VERTEX_POINT ( 'NONE', #21836 ) ;
#21942=FACE_OUTER_BOUND ( 'NONE', #18597, .T. ) ;
#21951=ORIENTED_EDGE ( 'NONE', *, *, #1516, .F. ) ;
#21952=DIRECTION ( 'NONE',  ( 0.000000000000000000, 0.000000000000000000, 1.000000000000000000 ) ) ;
#21958=VECTOR ( 'NONE', #4053, 1000.000000000000000 ) ;
#21964=DIRECTION ( 'NONE',  ( -0.000000000000000000, -0.000000000000000000, 1.000000000000000000 ) ) ;
#21965=CARTESIAN_POINT ( 'NONE',  ( -2.024999999999999911, -45.00000000000000000, -3.000000000000000000 ) ) ;
#21974=AXIS2_PLACEMENT_3D ( 'NONE', #2491, #11731, #9776 ) ;
#21980=AXIS2_PLACEMENT_3D ( 'NONE', #10059, #15677, #17513 ) ;
#21991=AXIS2_PLACEMENT_3D ( 'NONE', #14389, #7192, #5376 ) ;
#22001=DIRECTION ( 'NONE',  ( -0.000000000000000000, -0.000000000000000000, -1.000000000000000000 ) ) ;
#22010=DIRECTION ( 'NONE',  ( -1.000000000000000000, 0.000000000000000000, 0.000000000000000000 ) ) ;
#22021=ORIENTED_EDGE ( 'NONE', *, *, #6276, .F. ) ;
#22045=CIRCLE ( 'NONE', #1412, 8.000000000000000000 ) ;
#22054=ORIENTED_EDGE ( 'NONE', *, *, #8671, .T. ) ;
#22062=FACE_OUTER_BOUND ( 'NONE', #16029, .T. ) ;
#22066=VERTEX_POINT ( 'NONE', #20711 ) ;
#22090=DIRECTION ( 'NONE',  ( -0.000000000000000000, -0.000000000000000000, 1.000000000000000000 ) ) ;
#22095=DIRECTION ( 'NONE',  ( -0.000000000000000000, -0.000000000000000000, -1.000000000000000000 ) ) ;
#22099=EDGE_CURVE ( 'NONE', #11227, #16017, #20497, .T. ) ;
#22103=DIRECTION ( 'NONE',  ( -0.000000000000000000, -0.000000000000000000, 1.000000000000000000 ) ) ;
#22124=CARTESIAN_POINT ( 'NONE',  ( 35.99999999999999289, 50.99999999999999289, 0.5000000000000000000 ) ) ;
#22141=VERTEX_POINT ( 'NONE', #6448 ) ;
#22144=CIRCLE ( 'NONE', #14333, 15.00000000000000000 ) ;
#22147=EDGE_LOOP ( 'NONE', ( #8983, #3667, #2973, #23865 ) ) ;
#22148=PLANE ( 'NONE',  #13449 ) ;
#22160=CARTESIAN_POINT ( 'NONE',  ( 40.49999999999998579, 50.99999999999999289, 12.50000000000000000 ) ) ;
#22171=ADVANCED_FACE ( 'NONE', ( #17529 ), #8240, .T. ) ;
#22186=CARTESIAN_POINT ( 'NONE',  ( 35.99999999999999289, -51.00000000000000711, 0.000000000000000000 ) ) ;
#22188=CARTESIAN_POINT ( 'NONE',  ( 0.000000000000000000, 45.00000000000000000, -3.000000000000000000 ) ) ;
#22190=FACE_OUTER_BOUND ( 'NONE', #6567, .T. ) ;
#22195=VERTEX_POINT ( 'NONE', #4368 ) ;
#22197=ORIENTED_EDGE ( 'NONE', *, *, #11534, .F. ) ;
#22201=CARTESIAN_POINT ( 'NONE',  ( 28.99999999999999645, 29.49999999999999645, -3.000000000000000000 ) ) ;
#22203=VECTOR ( 'NONE', #11760, 1000.000000000000000 ) ;
#22209=CARTESIAN_POINT ( 'NONE',  ( 30.68762588338048403, 45.64284848299539732, -3.000000000000000000 ) ) ;
#22213=FACE_OUTER_BOUND ( 'NONE', #2655, .T. ) ;
#22217=ORIENTED_EDGE ( 'NONE', *, *, #12616, .T. ) ;
#22223=CARTESIAN_POINT ( 'NONE',  ( 29.00000000000000355, -29.50000000000000000, -3.000000000000000000 ) ) ;
#22227=EDGE_CURVE ( 'NONE', #16565, #1485, #15799, .T. ) ;
#22233=CARTESIAN_POINT ( 'NONE',  ( -9.999999999999998224, 15.50000000000000178, 7.699999999999998401 ) ) ;
#22237=ORIENTED_EDGE ( 'NONE', *, *, #13263, .F. ) ;
#22239=CARTESIAN_POINT ( 'NONE',  ( -28.99999999999999645, -29.50000000000000000, -2.224999999999995204 ) ) ;
#22249=VERTEX_POINT ( 'NONE', #14198 ) ;
#22262=AXIS2_PLACEMENT_3D ( 'NONE', #6291, #5930, #13736 ) ;
#22263=LINE ( 'NONE', #16396, #11096 ) ;
#22265=LINE ( 'NONE', #9307, #7574 ) ;
#22266=EDGE_CURVE ( 'NONE', #15606, #17955, #23834, .T. ) ;
#22273=EDGE_LOOP ( 'NONE', ( #6937, #8397, #10269, #17587 ) ) ;
#22278=AXIS2_PLACEMENT_3D ( 'NONE', #16360, #23819, #1613 ) ;
#22284=CARTESIAN_POINT ( 'NONE',  ( 29.00000000000000355, -29.50000000000000000, -3.000000000000000000 ) ) ;
#22295=CYLINDRICAL_SURFACE ( 'NONE', #7841, 1.999999999999996669 ) ;
#22299=CARTESIAN_POINT ( 'NONE',  ( -30.32370777929697425, -42.16181938034195298, 0.000000000000000000 ) ) ;
#22307=ORIENTED_EDGE ( 'NONE', *, *, #9580, .T. ) ;
#22310=ORIENTED_EDGE ( 'NONE', *, *, #19217, .T. ) ;
#22326=CARTESIAN_POINT ( 'NONE',  ( -44.00000000000000711, -51.00000000000000711, 0.000000000000000000 ) ) ;
#22335=DIRECTION ( 'NONE',  ( -1.000000000000000000, 0.000000000000000000, 0.000000000000000000 ) ) ;
#22341=AXIS2_PLACEMENT_3D ( 'NONE', #4414, #13929, #8291 ) ;
#22342=VECTOR ( 'NONE', #8835, 1000.000000000000000 ) ;
#22344=DIRECTION ( 'NONE',  ( 0.000000000000000000, 0.000000000000000000, 1.000000000000000000 ) ) ;
#22353=ORIENTED_EDGE ( 'NONE', *, *, #13954, .F. ) ;
#22355=ORIENTED_EDGE ( 'NONE', *, *, #21425, .T. ) ;
#22356=CIRCLE ( 'NONE', #2081, 8.999999999999994671 ) ;
#22369=CARTESIAN_POINT ( 'NONE',  ( 0.000000000000000000, 15.50000000000000000, 7.700000000000001954 ) ) ;
#22379=AXIS2_PLACEMENT_3D ( 'NONE', #13840, #21288, #11730 ) ;
#22380=ORIENTED_EDGE ( 'NONE', *, *, #19540, .F. ) ;
#22382=EDGE_CURVE ( 'NONE', #19429, #15518, #1170, .T. ) ;
#22387=DIRECTION ( 'NONE',  ( -1.000000000000000000, 0.000000000000000000, 0.000000000000000000 ) ) ;
#22389=CARTESIAN_POINT ( 'NONE',  ( -40.23082370883258108, -27.62204025492846071, -3.000000000000000000 ) ) ;
#22395=CARTESIAN_POINT ( 'NONE',  ( 30.32370777929699202, 42.16181938034194587, -1.500000000000000000 ) ) ;
#22406=VECTOR ( 'NONE', #8962, 1000.000000000000114 ) ;
#22412=CIRCLE ( 'NONE', #11866, 1.499999999999998002 ) ;
#22416=PLANE ( 'NONE',  #8887 ) ;
#22417=EDGE_CURVE ( 'NONE', #18344, #13385, #20145, .T. ) ;
#22424=VERTEX_POINT ( 'NONE', #23730 ) ;
#22445=EDGE_CURVE ( 'NONE', #4924, #11720, #14668, .T. ) ;
#22448=DIRECTION ( 'NONE',  ( -0.000000000000000000, -0.000000000000000000, -1.000000000000000000 ) ) ;
#22457=AXIS2_PLACEMENT_3D ( 'NONE', #13918, #21361, #4651 ) ;
#22458=CARTESIAN_POINT ( 'NONE',  ( 42.00000000000000000, 25.22443390181681622, -1.500000000000000000 ) ) ;
#22461=FACE_OUTER_BOUND ( 'NONE', #1165, .T. ) ;
#22467=ORIENTED_EDGE ( 'NONE', *, *, #21850, .T. ) ;
#22470=DIRECTION ( 'NONE',  ( -1.000000000000000000, 0.000000000000000000, 0.000000000000000000 ) ) ;
#22474=CARTESIAN_POINT ( 'NONE',  ( -35.99999999999995026, 59.99999999999998579, 0.000000000000000000 ) ) ;
#22475=EDGE_CURVE ( 'NONE', #8263, #3022, #13198, .T. ) ;
#22478=AXIS2_PLACEMENT_3D ( 'NONE', #6706, #8634, #17686 ) ;
#22481=DIRECTION ( 'NONE',  ( -0.000000000000000000, 0.000000000000000000, 1.000000000000000000 ) ) ;
#22489=FACE_BOUND ( 'NONE', #15076, .T. ) ;
#22493=DIRECTION ( 'NONE',  ( -1.000000000000000000, 0.000000000000000000, 0.000000000000000000 ) ) ;
#22506=CARTESIAN_POINT ( 'NONE',  ( 35.99999999999999289, 50.99999999999999289, 12.50000000000000000 ) ) ;
#22509=LINE ( 'NONE', #13585, #15639 ) ;
#22510=CARTESIAN_POINT ( 'NONE',  ( -34.02499999999999858, -29.50000000000000000, -3.000000000000000000 ) ) ;
#22521=ORIENTED_EDGE ( 'NONE', *, *, #9987, .T. ) ;
#22531=CARTESIAN_POINT ( 'NONE',  ( 30.16774287754692807, 40.66994976491903913, -3.000000000000000000 ) ) ;
#22532=DIRECTION ( 'NONE',  ( -0.000000000000000000, -0.000000000000000000, -1.000000000000000000 ) ) ;
#22533=DIRECTION ( 'NONE',  ( 0.000000000000000000, 0.000000000000000000, -1.000000000000000000 ) ) ;
#22537=EDGE_LOOP ( 'NONE', ( #18836, #17790 ) ) ;
#22539=ORIENTED_EDGE ( 'NONE', *, *, #18708, .F. ) ;
#22547=ADVANCED_FACE ( 'NONE', ( #1980, #14685 ), #22148, .T. ) ;
#22552=DIRECTION ( 'NONE',  ( -0.000000000000000000, -0.000000000000000000, -1.000000000000000000 ) ) ;
#22553=LINE ( 'NONE', #9601, #4127 ) ;
#22558=FACE_OUTER_BOUND ( 'NONE', #12764, .T. ) ;
#22569=EDGE_CURVE ( 'NONE', #10096, #10996, #3003, .T. ) ;
#22579=ORIENTED_EDGE ( 'NONE', *, *, #8113, .F. ) ;
#22597=EDGE_CURVE ( 'NONE', #15649, #22724, #13452, .T. ) ;
#22598=DIRECTION ( 'NONE',  ( -0.000000000000000000, -0.000000000000000000, -1.000000000000000000 ) ) ;
#22614=EDGE_CURVE ( 'NONE', #16185, #13109, #523, .T. ) ;
#22623=DIRECTION ( 'NONE',  ( 0.7052211081716915908, -0.7089874389501490404, 0.000000000000000000 ) ) ;
#22627=ORIENTED_EDGE ( 'NONE', *, *, #7082, .F. ) ;
#22629=ORIENTED_EDGE ( 'NONE', *, *, #16755, .T. ) ;
#22635=DIRECTION ( 'NONE',  ( -0.8571673007021121116, 0.000000000000000000, -0.5150380749100544886 ) ) ;
#22651=DIRECTION ( 'NONE',  ( -0.7052211081716895924, -0.7089874389501509278, 0.000000000000000000 ) ) ;
#22652=CYLINDRICAL_SURFACE ( 'NONE', #6831, 4.499999999999997335 ) ;
#22657=CONICAL_SURFACE ( 'NONE', #3559, 1.999999999999996669, 1.029744258676653867 ) ;
#22660=EDGE_LOOP ( 'NONE', ( #22579, #2978 ) ) ;
#22674=CARTESIAN_POINT ( 'NONE',  ( 29.00000000000000000, 29.50000000000000000, -3.000000000000000000 ) ) ;
#22695=DIRECTION ( 'NONE',  ( -1.000000000000000000, 0.000000000000000000, 0.000000000000000000 ) ) ;
#22703=AXIS2_PLACEMENT_3D ( 'NONE', #12152, #23415, #10198 ) ;
#22704=FACE_BOUND ( 'NONE', #5521, .T. ) ;
#22724=VERTEX_POINT ( 'NONE', #4309 ) ;
#22731=ADVANCED_FACE ( 'NONE', ( #2470 ), #6056, .F. ) ;
#22738=DIRECTION ( 'NONE',  ( -0.000000000000000000, -0.000000000000000000, -1.000000000000000000 ) ) ;
#22746=DIRECTION ( 'NONE',  ( 0.1039766011667100087, 0.9945797436152714610, 0.000000000000000000 ) ) ;
#22747=ORIENTED_EDGE ( 'NONE', *, *, #22445, .T. ) ;
#22748=AXIS2_PLACEMENT_3D ( 'NONE', #5991, #12062, #15742 ) ;
#22751=ORIENTED_EDGE ( 'NONE', *, *, #13188, .F. ) ;
#22756=CIRCLE ( 'NONE', #12602, 1.499999999999999778 ) ;
#22758=CIRCLE ( 'NONE', #23539, 5.000000000000000888 ) ;
#22759=LINE ( 'NONE', #6739, #11076 ) ;
#22760=EDGE_CURVE ( 'NONE', #16878, #2783, #10014, .T. ) ;
#22768=LINE ( 'NONE', #11633, #23932 ) ;
#22769=CYLINDRICAL_SURFACE ( 'NONE', #6481, 4.249999999999996447 ) ;
#22772=EDGE_CURVE ( 'NONE', #779, #4606, #21634, .T. ) ;
#22776=CONICAL_SURFACE ( 'NONE', #17312, 1.999999999999996669, 1.029744258676653867 ) ;
#22785=ORIENTED_EDGE ( 'NONE', *, *, #13105, .T. ) ;
#22788=ORIENTED_EDGE ( 'NONE', *, *, #21425, .F. ) ;
#22799=AXIS2_PLACEMENT_3D ( 'NONE', #6204, #7887, #5839 ) ;
#22815=ORIENTED_EDGE ( 'NONE', *, *, #1233, .F. ) ;
#22825=VECTOR ( 'NONE', #18362, 1000.000000000000000 ) ;
#22835=VECTOR ( 'NONE', #5273, 1000.000000000000000 ) ;
#22836=FACE_BOUND ( 'NONE', #9463, .T. ) ;
#22856=LINE ( 'NONE', #290, #12713 ) ;
#22865=ORIENTED_EDGE ( 'NONE', *, *, #17666, .T. ) ;
#22875=CARTESIAN_POINT ( 'NONE',  ( 30.16774287754692807, 40.66994976491903913, -3.000000000000000000 ) ) ;
#22876=CARTESIAN_POINT ( 'NONE',  ( 35.99999999999999289, 50.99999999999999289, 12.50000000000000000 ) ) ;
#22879=CARTESIAN_POINT ( 'NONE',  ( -28.99999999999999645, -29.50000000000000000, -3.000000000000000000 ) ) ;
#22890=VERTEX_POINT ( 'NONE', #23353 ) ;
#22893=ORIENTED_EDGE ( 'NONE', *, *, #3941, .T. ) ;
#22905=DIRECTION ( 'NONE',  ( 0.000000000000000000, 0.000000000000000000, -1.000000000000000000 ) ) ;
#22908=DIRECTION ( 'NONE',  ( -1.000000000000000000, 0.000000000000000000, 0.000000000000000000 ) ) ;
#22915=EDGE_CURVE ( 'NONE', #5565, #17524, #14059, .T. ) ;
#22924=CARTESIAN_POINT ( 'NONE',  ( 41.73082370883257397, -27.62204025492843940, 0.000000000000000000 ) ) ;
#22932=DIRECTION ( 'NONE',  ( -0.000000000000000000, -0.000000000000000000, -1.000000000000000000 ) ) ;
#22948=FACE_OUTER_BOUND ( 'NONE', #17097, .T. ) ;
#22951=DIRECTION ( 'NONE',  ( -1.000000000000000000, 0.000000000000000000, 0.000000000000000000 ) ) ;
#22953=DIRECTION ( 'NONE',  ( 0.000000000000000000, -1.000000000000000000, 0.000000000000000000 ) ) ;
#22971=EDGE_CURVE ( 'NONE', #13127, #1485, #16929, .T. ) ;
#22989=CARTESIAN_POINT ( 'NONE',  ( -35.99999999999995026, 59.99999999999998579, 12.50000000000000000 ) ) ;
#23008=CARTESIAN_POINT ( 'NONE',  ( -28.99999999999999645, 29.50000000000000000, -2.224999999999995204 ) ) ;
#23011=VERTEX_POINT ( 'NONE', #11419 ) ;
#23013=CARTESIAN_POINT ( 'NONE',  ( 44.99999999999998579, 50.99999999999992184, 12.50000000000000000 ) ) ;
#23015=EDGE_CURVE ( 'NONE', #10096, #13428, #22553, .T. ) ;
#23019=LINE ( 'NONE', #4492, #18118 ) ;
#23022=ORIENTED_EDGE ( 'NONE', *, *, #3129, .T. ) ;
#23023=ORIENTED_EDGE ( 'NONE', *, *, #5985, .F. ) ;
#23035=CARTESIAN_POINT ( 'NONE',  ( -43.50000000000000711, 25.22443390181683043, -1.500000000000000000 ) ) ;
#23037=CARTESIAN_POINT ( 'NONE',  ( -41.99999999999996447, -25.22443390181684464, -0.6213203435596427182 ) ) ;
#23038=ADVANCED_FACE ( 'NONE', ( #14527 ), #5950, .F. ) ;
#23042=EDGE_CURVE ( 'NONE', #7111, #1863, #21669, .T. ) ;
#23043=ORIENTED_EDGE ( 'NONE', *, *, #5193, .F. ) ;
#23057=EDGE_CURVE ( 'NONE', #12524, #910, #9711, .T. ) ;
#23064=EDGE_LOOP ( 'NONE', ( #18983, #7514, #9899, #3177 ) ) ;
#23068=ORIENTED_EDGE ( 'NONE', *, *, #14404, .F. ) ;
#23069=CYLINDRICAL_SURFACE ( 'NONE', #15219, 5.000000000000004441 ) ;
#23074=CARTESIAN_POINT ( 'NONE',  ( -36.00000000000000711, -51.00000000000000711, 12.50000000000000000 ) ) ;
#23108=CARTESIAN_POINT ( 'NONE',  ( 33.25000000000000000, -29.50000000000000000, -2.224999999999995204 ) ) ;
#23110=DIRECTION ( 'NONE',  ( -0.000000000000000000, -0.000000000000000000, -1.000000000000000000 ) ) ;
#23112=CARTESIAN_POINT ( 'NONE',  ( -39.49999999999998579, 15.50000000000000000, 19.70000000000000284 ) ) ;
#23113=DIRECTION ( 'NONE',  ( -1.000000000000000000, 0.000000000000000000, 0.000000000000000000 ) ) ;
#23122=ORIENTED_EDGE ( 'NONE', *, *, #1857, .F. ) ;
#23135=VERTEX_POINT ( 'NONE', #22924 ) ;
#23137=DIRECTION ( 'NONE',  ( -0.000000000000000000, -0.000000000000000000, -1.000000000000000000 ) ) ;
#23151=CYLINDRICAL_SURFACE ( 'NONE', #21980, 11.23082370883260417 ) ;
#23170=VECTOR ( 'NONE', #23598, 1000.000000000000000 ) ;
#23181=ORIENTED_EDGE ( 'NONE', *, *, #1, .T. ) ;
#23191=ADVANCED_FACE ( 'NONE', ( #2407 ), #14006, .F. ) ;
#23193=DIRECTION ( 'NONE',  ( -1.000000000000000000, 0.000000000000000000, 0.000000000000000000 ) ) ;
#23194=EDGE_CURVE ( 'NONE', #16878, #2131, #15404, .T. ) ;
#23199=DIRECTION ( 'NONE',  ( 0.000000000000000000, -0.000000000000000000, 1.000000000000000000 ) ) ;
#23210=ORIENTED_EDGE ( 'NONE', *, *, #15159, .T. ) ;
#23213=CARTESIAN_POINT ( 'NONE',  ( -41.73082370883260239, 27.62204025492845361, -1.500000000000000000 ) ) ;
#23233=AXIS2_PLACEMENT_3D ( 'NONE', #11757, #19232, #2515 ) ;
#23236=ORIENTED_EDGE ( 'NONE', *, *, #24079, .F. ) ;
#23239=CARTESIAN_POINT ( 'NONE',  ( 41.73082370883260239, 27.62204025492843940, -1.500000000000000000 ) ) ;
#23241=DIRECTION ( 'NONE',  ( -1.000000000000000000, 0.000000000000000000, 0.000000000000000000 ) ) ;
#23242=ORIENTED_EDGE ( 'NONE', *, *, #5193, .T. ) ;
#23245=CARTESIAN_POINT ( 'NONE',  ( 1.999999999999996669, 45.00000000000000000, -8.673617379884035472E-16 ) ) ;
#23248=CIRCLE ( 'NONE', #253, 5.025000000000002132 ) ;
#23252=FACE_OUTER_BOUND ( 'NONE', #5888, .T. ) ;
#23253=FACE_OUTER_BOUND ( 'NONE', #15285, .T. ) ;
#23255=VECTOR ( 'NONE', #12451, 1000.000000000000000 ) ;
#23257=EDGE_LOOP ( 'NONE', ( #21651, #20423 ) ) ;
#23258=EDGE_LOOP ( 'NONE', ( #16753, #23414, #7735, #19960, #22217, #10302, #2059, #10647 ) ) ;
#23262=ORIENTED_EDGE ( 'NONE', *, *, #5824, .T. ) ;
#23269=EDGE_LOOP ( 'NONE', ( #6867, #6160, #6057, #23068 ) ) ;
#23284=CIRCLE ( 'NONE', #4183, 4.250000000000000000 ) ;
#23302=LINE ( 'NONE', #21812, #20754 ) ;
#23307=DIRECTION ( 'NONE',  ( 1.000000000000000000, 0.000000000000000000, 0.000000000000000000 ) ) ;
#23314=ORIENTED_EDGE ( 'NONE', *, *, #22760, .T. ) ;
#23320=VECTOR ( 'NONE', #8071, 999.9999999999998863 ) ;
#23321=DIRECTION ( 'NONE',  ( -0.7071067811865292541, 0.000000000000000000, -0.7071067811865658914 ) ) ;
#23327=DIRECTION ( 'NONE',  ( 0.000000000000000000, 0.000000000000000000, -1.000000000000000000 ) ) ;
#23334=AXIS2_PLACEMENT_3D ( 'NONE', #23764, #21925, #12642 ) ;
#23338=DIRECTION ( 'NONE',  ( -1.000000000000000000, 0.000000000000000000, 0.000000000000000000 ) ) ;
#23343=ORIENTED_EDGE ( 'NONE', *, *, #18999, .T. ) ;
#23353=CARTESIAN_POINT ( 'NONE',  ( 35.99999999999992184, 59.99999999999998579, 12.50000000000000000 ) ) ;
#23356=EDGE_LOOP ( 'NONE', ( #2196, #17010, #14022, #20126 ) ) ;
#23360=ORIENTED_EDGE ( 'NONE', *, *, #6908, .F. ) ;
#23368=EDGE_CURVE ( 'NONE', #6097, #7176, #20518, .T. ) ;
#23369=SPHERICAL_SURFACE ( 'NONE', #2032, 1.500000000000000000 ) ;
#23387=EDGE_LOOP ( 'NONE', ( #4454, #15185, #1524, #6195 ) ) ;
#23414=ORIENTED_EDGE ( 'NONE', *, *, #12549, .T. ) ;
#23415=DIRECTION ( 'NONE',  ( -0.000000000000000000, -0.000000000000000000, -1.000000000000000000 ) ) ;
#23433=DIRECTION ( 'NONE',  ( 0.000000000000000000, 0.000000000000000000, -1.000000000000000000 ) ) ;
#23450=ORIENTED_EDGE ( 'NONE', *, *, #7536, .F. ) ;
#23463=ADVANCED_FACE ( 'NONE', ( #11522 ), #22769, .F. ) ;
#23465=EDGE_LOOP ( 'NONE', ( #5331, #429 ) ) ;
#23466=LINE ( 'NONE', #16135, #23170 ) ;
#23478=ORIENTED_EDGE ( 'NONE', *, *, #14811, .F. ) ;
#23480=DIRECTION ( 'NONE',  ( 1.000000000000000000, 0.000000000000000000, 0.000000000000000000 ) ) ;
#23481=DIRECTION ( 'NONE',  ( 0.000000000000000000, 0.000000000000000000, 1.000000000000000000 ) ) ;
#23490=DIRECTION ( 'NONE',  ( -0.000000000000000000, -0.000000000000000000, -1.000000000000000000 ) ) ;
#23513=EDGE_CURVE ( 'NONE', #4806, #5924, #3609, .T. ) ;
#23517=AXIS2_PLACEMENT_3D ( 'NONE', #3644, #7405, #14847 ) ;
#23521=ORIENTED_EDGE ( 'NONE', *, *, #1725, .T. ) ;
#23526=LINE ( 'NONE', #19756, #5604 ) ;
#23531=AXIS2_PLACEMENT_3D ( 'NONE', #15273, #6263, #23113 ) ;
#23532=DIRECTION ( 'NONE',  ( -1.000000000000000000, 0.000000000000000000, 0.000000000000000000 ) ) ;
#23539=AXIS2_PLACEMENT_3D ( 'NONE', #18265, #11150, #9322 ) ;
#23542=EDGE_LOOP ( 'NONE', ( #261, #12307 ) ) ;
#23562=LINE ( 'NONE', #16226, #1642 ) ;
#23564=CARTESIAN_POINT ( 'NONE',  ( 35.99999999999999289, -51.00000000000000711, 12.50000000000000000 ) ) ;
#23570=CIRCLE ( 'NONE', #21991, 8.000000000000000000 ) ;
#23580=ORIENTED_EDGE ( 'NONE', *, *, #22475, .F. ) ;
#23583=DIRECTION ( 'NONE',  ( -0.000000000000000000, -0.000000000000000000, -1.000000000000000000 ) ) ;
#23596=AXIS2_PLACEMENT_3D ( 'NONE', #564, #15297, #11754 ) ;
#23598=DIRECTION ( 'NONE',  ( 1.000000000000000000, 0.000000000000000000, 0.000000000000000000 ) ) ;
#23600=VECTOR ( 'NONE', #17061, 999.9999999999998863 ) ;
#23609=DIRECTION ( 'NONE',  ( 1.000000000000000000, 0.000000000000000000, 0.000000000000000000 ) ) ;
#23611=DIRECTION ( 'NONE',  ( 0.000000000000000000, -0.000000000000000000, 1.000000000000000000 ) ) ;
#23614=DIRECTION ( 'NONE',  ( -0.000000000000000000, -0.000000000000000000, -1.000000000000000000 ) ) ;
#23616=AXIS2_PLACEMENT_3D ( 'NONE', #62, #18138, #12850 ) ;
#23625=EDGE_LOOP ( 'NONE', ( #10036, #1061, #6096, #4932 ) ) ;
#23632=EDGE_CURVE ( 'NONE', #4705, #19429, #9566, .T. ) ;
#23642=CARTESIAN_POINT ( 'NONE',  ( 43.50000000000000711, 25.22443390181681622, -1.500000000000000000 ) ) ;
#23645=ORIENTED_EDGE ( 'NONE', *, *, #15502, .T. ) ;
#23651=CARTESIAN_POINT ( 'NONE',  ( 30.68762588338046982, -45.64284848299539732, -3.000000000000000000 ) ) ;
#23661=ORIENTED_EDGE ( 'NONE', *, *, #12674, .T. ) ;
#23669=ORIENTED_EDGE ( 'NONE', *, *, #13025, .T. ) ;
#23674=ORIENTED_EDGE ( 'NONE', *, *, #23958, .T. ) ;
#23686=EDGE_CURVE ( 'NONE', #13385, #2874, #563, .T. ) ;
#23688=DIRECTION ( 'NONE',  ( -0.000000000000000000, -0.000000000000000000, 1.000000000000000000 ) ) ;
#23697=DIRECTION ( 'NONE',  ( -0.000000000000000000, -0.000000000000000000, -1.000000000000000000 ) ) ;
#23699=DIRECTION ( 'NONE',  ( 0.000000000000000000, 0.000000000000000000, 1.000000000000000000 ) ) ;
#23706=VERTEX_POINT ( 'NONE', #7570 ) ;
#23708=CARTESIAN_POINT ( 'NONE',  ( 1.999999999999996669, -45.00000000000000000, -8.673617379884035472E-16 ) ) ;
#23719=CYLINDRICAL_SURFACE ( 'NONE', #9084, 40.00000000000000000 ) ;
#23729=EDGE_LOOP ( 'NONE', ( #13470, #10580 ) ) ;
#23730=CARTESIAN_POINT ( 'NONE',  ( -28.00000000000000355, -51.00000000000000711, 0.5000000000000000000 ) ) ;
#23738=ORIENTED_EDGE ( 'NONE', *, *, #8520, .T. ) ;
#23743=EDGE_CURVE ( 'NONE', #11720, #13291, #18696, .T. ) ;
#23748=FACE_OUTER_BOUND ( 'NONE', #9391, .T. ) ;
#23762=EDGE_CURVE ( 'NONE', #18287, #23864, #22856, .T. ) ;
#23764=CARTESIAN_POINT ( 'NONE',  ( -41.73082370883260239, 27.62204025492845361, -1.500000000000000000 ) ) ;
#23768=DIRECTION ( 'NONE',  ( -1.000000000000000000, 0.000000000000000000, 0.000000000000000000 ) ) ;
#23770=LINE ( 'NONE', #5221, #15702 ) ;
#23773=PLANE ( 'NONE',  #9428 ) ;
#23783=CARTESIAN_POINT ( 'NONE',  ( -36.00000000000001421, 50.99999999999999289, 12.50000000000000000 ) ) ;
#23788=EDGE_CURVE ( 'NONE', #978, #6856, #15844, .T. ) ;
#23789=DIRECTION ( 'NONE',  ( -0.000000000000000000, -0.000000000000000000, -1.000000000000000000 ) ) ;
#23791=CARTESIAN_POINT ( 'NONE',  ( -40.66734255040736201, -26.56420859267092283, -3.000000000000000000 ) ) ;
#23816=EDGE_LOOP ( 'NONE', ( #126, #12597, #1441 ) ) ;
#23819=DIRECTION ( 'NONE',  ( -0.000000000000000000, -0.000000000000000000, -1.000000000000000000 ) ) ;
#23820=ORIENTED_EDGE ( 'NONE', *, *, #2232, .T. ) ;
#23834=LINE ( 'NONE', #4958, #18572 ) ;
#23836=LINE ( 'NONE', #1419, #22342 ) ;
#23853=ORIENTED_EDGE ( 'NONE', *, *, #10545, .F. ) ;
#23861=VECTOR ( 'NONE', #20792, 1000.000000000000000 ) ;
#23864=VERTEX_POINT ( 'NONE', #15886 ) ;
#23865=ORIENTED_EDGE ( 'NONE', *, *, #22445, .F. ) ;
#23874=ORIENTED_EDGE ( 'NONE', *, *, #24078, .T. ) ;
#23884=CIRCLE ( 'NONE', #7480, 11.23082370883260417 ) ;
#23886=DIRECTION ( 'NONE',  ( -0.000000000000000000, -0.000000000000000000, -1.000000000000000000 ) ) ;
#23887=EDGE_LOOP ( 'NONE', ( #23738, #17673, #3930, #22521 ) ) ;
#23891=AXIS2_PLACEMENT_3D ( 'NONE', #16890, #7842, #11257 ) ;
#23893=ORIENTED_EDGE ( 'NONE', *, *, #1162, .F. ) ;
#23904=VECTOR ( 'NONE', #19478, 1000.000000000000000 ) ;
#23911=CARTESIAN_POINT ( 'NONE',  ( 40.49999999999998579, -51.00000000000000711, 12.50000000000000000 ) ) ;
#23913=AXIS2_PLACEMENT_3D ( 'NONE', #16928, #3413, #1704 ) ;
#23916=DIRECTION ( 'NONE',  ( -0.000000000000000000, -0.000000000000000000, -1.000000000000000000 ) ) ;
#23923=ADVANCED_FACE ( 'NONE', ( #764, #12075 ), #883, .T. ) ;
#23924=ORIENTED_EDGE ( 'NONE', *, *, #5570, .F. ) ;
#23925=DIRECTION ( 'NONE',  ( 1.000000000000000000, 0.000000000000000000, 0.000000000000000000 ) ) ;
#23932=VECTOR ( 'NONE', #11521, 1000.000000000000114 ) ;
#23938=CARTESIAN_POINT ( 'NONE',  ( 31.49999999999999289, 50.99999999999999289, 0.5000000000000004441 ) ) ;
#23943=ORIENTED_EDGE ( 'NONE', *, *, #1498, .F. ) ;
#23945=FACE_OUTER_BOUND ( 'NONE', #21401, .T. ) ;
#23952=DIRECTION ( 'NONE',  ( -0.000000000000000000, -0.000000000000000000, -1.000000000000000000 ) ) ;
#23957=FACE_OUTER_BOUND ( 'NONE', #1841, .T. ) ;
#23958=EDGE_CURVE ( 'NONE', #12988, #15606, #23284, .T. ) ;
#23969=DIRECTION ( 'NONE',  ( -0.000000000000000000, -0.000000000000000000, 1.000000000000000000 ) ) ;
#23982=EDGE_LOOP ( 'NONE', ( #17220, #3336, #1022, #17402 ) ) ;
#23983=AXIS2_PLACEMENT_3D ( 'NONE', #20989, #11574, #13416 ) ;
#23991=LINE ( 'NONE', #14934, #1380 ) ;
#23999=LINE ( 'NONE', #3858, #2911 ) ;
#24034=FACE_OUTER_BOUND ( 'NONE', #23816, .T. ) ;
#24043=ORIENTED_EDGE ( 'NONE', *, *, #17919, .T. ) ;
#24055=CARTESIAN_POINT ( 'NONE',  ( 27.89784171216406961, 41.49349862090490859, -1.500000000000000000 ) ) ;
#24062=ORIENTED_EDGE ( 'NONE', *, *, #17125, .F. ) ;
#24067=ORIENTED_EDGE ( 'NONE', *, *, #268, .F. ) ;
#24078=EDGE_CURVE ( 'NONE', #3028, #19491, #11357, .T. ) ;
#24079=EDGE_CURVE ( 'NONE', #12610, #9321, #17011, .T. ) ;
#24080=CARTESIAN_POINT ( 'NONE',  ( 40.23082370883257397, -29.49999999999999645, -3.000000000000000000 ) ) ;
#24082=CARTESIAN_POINT ( 'NONE',  ( 0.000000000000000000, 45.00000000000000000, -8.673617379884035472E-16 ) ) ;
#24083=DIRECTION ( 'NONE',  ( -1.000000000000000000, 0.000000000000000000, 0.000000000000000000 ) ) ;
#24086=DIRECTION ( 'NONE',  ( 1.000000000000000000, 0.000000000000000000, 0.000000000000000000 ) ) ;
#24095=ORIENTED_EDGE ( 'NONE', *, *, #8497, .F. ) ;
#24135=COLOUR_RGB('Light Blue',0.38,0.62,0.78);
#24136=FILL_AREA_STYLE_COLOUR('',#24135);
#24137=FILL_AREA_STYLE('',(#24136));
#24138=SURFACE_STYLE_FILL_AREA(#24137);
#24139=SURFACE_SIDE_STYLE('',(#24138));
#24140=SURFACE_STYLE_USAGE(.BOTH.,#24139);
#24141=PRESENTATION_STYLE_ASSIGNMENT((#24140));
ENDSEC;
END-ISO-10303-21;
